ISO-10303-21;
HEADER;
/* Generated by software containing ST-Developer
 * from STEP Tools, Inc. (www.steptools.com) 
 */

FILE_DESCRIPTION(
/* description */ ('Independent keyed three-contact power inlet for the IEC-connector des
ign category. Longer ground blade, retained contacts, wire termination
 holes and sealed bolted panel interface. Nominal custom interface; IE
C dimensional compatibility and electrical ratings are not assigned.'),

/* implementation_level */ '2;1');

FILE_NAME(
/* name */ 'Hex nut M6.step',
/* time_stamp */ '2026-11-08T19:55:04-08:00',
/* author */ (''),
/* organization */ (''),
/* preprocessor_version */ 'ST-DEVELOPER v20.2',
/* originating_system */ 'Autodesk Translation Framework v15.17.0.0',
/* authorisation */ '');

FILE_SCHEMA (('AUTOMOTIVE_DESIGN { 1 0 10303 214 3 1 1 }'));
ENDSEC;

DATA;
#10=MECHANICAL_DESIGN_GEOMETRIC_PRESENTATION_REPRESENTATION('',(#118),#21880);
#98=SHAPE_REPRESENTATION_RELATIONSHIP('SRR','None',#21934,#108);
#108=ADVANCED_BREP_SHAPE_REPRESENTATION('',(#128),#21879);
#118=STYLED_ITEM('',(#21985),#128);
#128=MANIFOLD_SOLID_BREP('Body1',#6390);
#141=B_SPLINE_SURFACE_WITH_KNOTS('',3,3,((#21091,#21092,#21093,#21094,#21095,
#21096,#21097,#21098,#21099,#21100,#21101,#21102,#21103,#21104,#21105,#21106,
#21107,#21108,#21109,#21110,#21111,#21112,#21113,#21114,#21115,#21116,#21117,
#21118,#21119,#21120,#21121,#21122,#21123,#21124,#21125,#21126,#21127),
(#21128,#21129,#21130,#21131,#21132,#21133,#21134,#21135,#21136,#21137,
#21138,#21139,#21140,#21141,#21142,#21143,#21144,#21145,#21146,#21147,#21148,
#21149,#21150,#21151,#21152,#21153,#21154,#21155,#21156,#21157,#21158,#21159,
#21160,#21161,#21162,#21163,#21164),(#21165,#21166,#21167,#21168,#21169,
#21170,#21171,#21172,#21173,#21174,#21175,#21176,#21177,#21178,#21179,#21180,
#21181,#21182,#21183,#21184,#21185,#21186,#21187,#21188,#21189,#21190,#21191,
#21192,#21193,#21194,#21195,#21196,#21197,#21198,#21199,#21200,#21201),
(#21202,#21203,#21204,#21205,#21206,#21207,#21208,#21209,#21210,#21211,
#21212,#21213,#21214,#21215,#21216,#21217,#21218,#21219,#21220,#21221,#21222,
#21223,#21224,#21225,#21226,#21227,#21228,#21229,#21230,#21231,#21232,#21233,
#21234,#21235,#21236,#21237,#21238)),.UNSPECIFIED.,.F.,.F.,.F.,(4,4),(4,
1,1,1,1,1,1,1,1,1,1,1,1,1,1,1,1,1,1,1,1,1,1,1,1,1,1,1,1,1,1,1,1,1,4),(0.,
0.0642013499338864),(11.8589888623078,12.8423086102174,13.825628358127,
14.8089481060366,15.7922678539462,16.7755876018558,17.7589073497654,18.742227097675,
19.7255468455846,20.7088665934942,21.6921863414038,22.6755060893134,23.658825837223,
24.6421455851326,25.6254653330422,26.6087850809518,27.5921048288614,28.575424576771,
29.5587443246806,30.5420640725902,31.5253838204998,32.5087035684094,33.492023316319,
34.4753430642286,35.4586628121382,36.4419825600478,37.4253023079574,38.408622055867,
39.3919418037766,40.3752615516862,41.3585812995958,42.3419010475054,43.325220795415,
44.3085405433246,45.2918602912342),.UNSPECIFIED.);
#142=B_SPLINE_SURFACE_WITH_KNOTS('',3,3,((#21446,#21447,#21448,#21449,#21450,
#21451,#21452,#21453,#21454,#21455,#21456,#21457,#21458,#21459,#21460,#21461,
#21462,#21463,#21464,#21465,#21466,#21467,#21468,#21469,#21470,#21471,#21472,
#21473,#21474,#21475,#21476,#21477,#21478,#21479,#21480,#21481,#21482),
(#21483,#21484,#21485,#21486,#21487,#21488,#21489,#21490,#21491,#21492,
#21493,#21494,#21495,#21496,#21497,#21498,#21499,#21500,#21501,#21502,#21503,
#21504,#21505,#21506,#21507,#21508,#21509,#21510,#21511,#21512,#21513,#21514,
#21515,#21516,#21517,#21518,#21519),(#21520,#21521,#21522,#21523,#21524,
#21525,#21526,#21527,#21528,#21529,#21530,#21531,#21532,#21533,#21534,#21535,
#21536,#21537,#21538,#21539,#21540,#21541,#21542,#21543,#21544,#21545,#21546,
#21547,#21548,#21549,#21550,#21551,#21552,#21553,#21554,#21555,#21556),
(#21557,#21558,#21559,#21560,#21561,#21562,#21563,#21564,#21565,#21566,
#21567,#21568,#21569,#21570,#21571,#21572,#21573,#21574,#21575,#21576,#21577,
#21578,#21579,#21580,#21581,#21582,#21583,#21584,#21585,#21586,#21587,#21588,
#21589,#21590,#21591,#21592,#21593)),.UNSPECIFIED.,.F.,.F.,.F.,(4,4),(4,
1,1,1,1,1,1,1,1,1,1,1,1,1,1,1,1,1,1,1,1,1,1,1,1,1,1,1,1,1,1,1,1,1,4),(0.,
0.0642013499338863),(14.3984001269719,15.3817198748815,16.3650396227911,
17.3483593707007,18.3316791186103,19.3149988665199,20.2983186144295,21.2816383623391,
22.2649581102487,23.2482778581583,24.2315976060679,25.2149173539775,26.1982371018871,
27.1815568497966,28.1648765977063,29.1481963456159,30.1315160935254,31.114835841435,
32.0981555893446,33.0814753372542,34.0647950851639,35.0481148330734,36.031434580983,
37.0147543288926,37.9980740768022,38.9813938247118,39.9647135726214,40.948033320531,
41.9313530684406,42.9146728163502,43.8979925642598,44.8813123121694,45.864632060079,
46.8479518079886,47.8312715558982),.UNSPECIFIED.);
#195=FACE_BOUND('',#1057,.T.);
#196=FACE_BOUND('',#1066,.T.);
#305=PLANE('',#6941);
#306=PLANE('',#6943);
#307=PLANE('',#6944);
#308=PLANE('',#6945);
#309=PLANE('',#6946);
#310=PLANE('',#6947);
#311=PLANE('',#6948);
#312=PLANE('',#6949);
#647=FACE_OUTER_BOUND('',#1043,.T.);
#648=FACE_OUTER_BOUND('',#1044,.T.);
#649=FACE_OUTER_BOUND('',#1045,.T.);
#650=FACE_OUTER_BOUND('',#1046,.T.);
#651=FACE_OUTER_BOUND('',#1047,.T.);
#652=FACE_OUTER_BOUND('',#1048,.T.);
#653=FACE_OUTER_BOUND('',#1049,.T.);
#654=FACE_OUTER_BOUND('',#1050,.T.);
#655=FACE_OUTER_BOUND('',#1051,.T.);
#656=FACE_OUTER_BOUND('',#1052,.T.);
#657=FACE_OUTER_BOUND('',#1053,.T.);
#658=FACE_OUTER_BOUND('',#1054,.T.);
#659=FACE_OUTER_BOUND('',#1055,.T.);
#660=FACE_OUTER_BOUND('',#1056,.T.);
#661=FACE_OUTER_BOUND('',#1058,.T.);
#662=FACE_OUTER_BOUND('',#1059,.T.);
#663=FACE_OUTER_BOUND('',#1060,.T.);
#664=FACE_OUTER_BOUND('',#1061,.T.);
#665=FACE_OUTER_BOUND('',#1062,.T.);
#666=FACE_OUTER_BOUND('',#1063,.T.);
#667=FACE_OUTER_BOUND('',#1064,.T.);
#668=FACE_OUTER_BOUND('',#1065,.T.);
#1043=EDGE_LOOP('',(#5711,#5712,#5713,#5714));
#1044=EDGE_LOOP('',(#5715,#5716,#5717,#5718));
#1045=EDGE_LOOP('',(#5719,#5720,#5721,#5722));
#1046=EDGE_LOOP('',(#5723,#5724,#5725,#5726));
#1047=EDGE_LOOP('',(#5727,#5728,#5729,#5730));
#1048=EDGE_LOOP('',(#5731,#5732,#5733,#5734));
#1049=EDGE_LOOP('',(#5735,#5736,#5737,#5738));
#1050=EDGE_LOOP('',(#5739,#5740,#5741,#5742));
#1051=EDGE_LOOP('',(#5743,#5744,#5745,#5746));
#1052=EDGE_LOOP('',(#5747,#5748,#5749,#5750));
#1053=EDGE_LOOP('',(#5751,#5752,#5753,#5754));
#1054=EDGE_LOOP('',(#5755,#5756,#5757,#5758,#5759,#5760,#5761,#5762,#5763,
#5764,#5765,#5766,#5767,#5768));
#1055=EDGE_LOOP('',(#5769,#5770,#5771,#5772,#5773,#5774,#5775,#5776,#5777,
#5778,#5779,#5780,#5781,#5782));
#1056=EDGE_LOOP('',(#5783,#5784,#5785,#5786,#5787,#5788));
#1057=EDGE_LOOP('',(#5789,#5790,#5791,#5792));
#1058=EDGE_LOOP('',(#5793,#5794,#5795,#5796));
#1059=EDGE_LOOP('',(#5797,#5798,#5799,#5800));
#1060=EDGE_LOOP('',(#5801,#5802,#5803,#5804));
#1061=EDGE_LOOP('',(#5805,#5806,#5807,#5808));
#1062=EDGE_LOOP('',(#5809,#5810,#5811,#5812));
#1063=EDGE_LOOP('',(#5813,#5814,#5815,#5816));
#1064=EDGE_LOOP('',(#5817,#5818,#5819,#5820));
#1065=EDGE_LOOP('',(#5821,#5822,#5823,#5824,#5825,#5826));
#1066=EDGE_LOOP('',(#5827,#5828,#5829,#5830));
#1158=CIRCLE('',#6927,2.5175);
#1159=CIRCLE('',#6932,2.5175);
#1160=CIRCLE('',#6934,3.0735);
#1161=CIRCLE('',#6939,3.0735);
#1501=B_SPLINE_CURVE_WITH_KNOTS('',3,(#20749,#20750,#20751,#20752),
 .UNSPECIFIED.,.F.,.F.,(4,4),(32.725489676875,33.4328714289264),
 .UNSPECIFIED.);
#1502=B_SPLINE_CURVE_WITH_KNOTS('',3,(#20755,#20756,#20757,#20758,#20759,
#20760,#20761,#20762,#20763,#20764),.UNSPECIFIED.,.F.,.F.,(4,3,3,4),(-31.4159265358979,
-30.4829121851976,-29.499592437288,-28.9817156343595),.UNSPECIFIED.);
#1503=B_SPLINE_CURVE_WITH_KNOTS('',3,(#20769,#20770,#20771,#20772,#20773,
#20774,#20775,#20776,#20777,#20778,#20779,#20780,#20781,#20782,#20783,#20784,
#20785,#20786,#20787,#20788,#20789,#20790,#20791,#20792,#20793),
 .UNSPECIFIED.,.F.,.F.,(4,3,3,3,3,3,3,3,4),(26.4423043696954,26.5496331935592,
27.5329529414688,28.5162726893784,29.499592437288,30.4829121851976,31.4662319331072,
32.4495516810168,32.725489676875),.UNSPECIFIED.);
#1504=B_SPLINE_CURVE_WITH_KNOTS('',3,(#20794,#20795,#20796,#20797,#20798,
#20799,#20800,#20801,#20802,#20803,#20804,#20805,#20806,#20807,#20808,#20809,
#20810,#20811,#20812,#20813,#20814,#20815),.UNSPECIFIED.,.F.,.F.,(4,3,3,
3,3,3,3,4),(-28.9817156343595,-28.5162726893784,-27.5329529414688,-26.5496331935592,
-25.5663134456496,-24.58299369774,-23.5996739498304,-22.6985303271799),
 .UNSPECIFIED.);
#1505=B_SPLINE_CURVE_WITH_KNOTS('',3,(#20820,#20821,#20822,#20823,#20824,
#20825,#20826,#20827,#20828,#20829,#20830,#20831,#20832,#20833,#20834,#20835,
#20836,#20837,#20838,#20839,#20840,#20841),.UNSPECIFIED.,.F.,.F.,(4,3,3,
3,3,3,3,4),(20.1591190625159,20.6497147061016,21.6330344540112,22.6163542019208,
23.5996739498304,24.58299369774,25.5663134456496,26.4423043696954),
 .UNSPECIFIED.);
#1506=B_SPLINE_CURVE_WITH_KNOTS('',3,(#20842,#20843,#20844,#20845,#20846,
#20847,#20848,#20849,#20850,#20851,#20852,#20853,#20854,#20855,#20856,#20857,
#20858,#20859,#20860,#20861,#20862,#20863,#20864,#20865,#20866),
 .UNSPECIFIED.,.F.,.F.,(4,3,3,3,3,3,3,3,4),(-22.6985303271799,-22.6163542019208,
-21.6330344540112,-20.6497147061016,-19.666394958192,-18.6830752102824,
-17.6997554623728,-16.7164357144632,-16.4153450200003),.UNSPECIFIED.);
#1507=B_SPLINE_CURVE_WITH_KNOTS('',3,(#20871,#20872,#20873,#20874,#20875,
#20876,#20877,#20878,#20879,#20880,#20881,#20882,#20883,#20884,#20885,#20886,
#20887,#20888,#20889,#20890,#20891,#20892),.UNSPECIFIED.,.F.,.F.,(4,3,3,
3,3,3,3,4),(13.8759337553363,14.749796218644,15.7331159665536,16.7164357144632,
17.6997554623728,18.6830752102824,19.666394958192,20.1591190625159),
 .UNSPECIFIED.);
#1508=B_SPLINE_CURVE_WITH_KNOTS('',3,(#20893,#20894,#20895,#20896,#20897,
#20898,#20899,#20900,#20901,#20902,#20903,#20904,#20905,#20906,#20907,#20908,
#20909,#20910,#20911,#20912,#20913,#20914),.UNSPECIFIED.,.F.,.F.,(4,3,3,
3,3,3,3,4),(-16.4153450200003,-15.7331159665536,-14.749796218644,-13.7664764707344,
-12.7831567228248,-11.7998369749152,-10.8165172270056,-10.1321597128207),
 .UNSPECIFIED.);
#1509=B_SPLINE_CURVE_WITH_KNOTS('',3,(#20920,#20921,#20922,#20923,#20924,
#20925,#20926,#20927,#20928,#20929,#20930,#20931,#20932),.UNSPECIFIED.,
 .F.,.F.,(4,3,3,3,4),(-3.84897440564114,-2.9499592437288,-1.9666394958192,
-0.983319747909601,0.),.UNSPECIFIED.);
#1510=B_SPLINE_CURVE_WITH_KNOTS('',3,(#20935,#20936,#20937,#20938,#20939,
#20940,#20941,#20942,#20943,#20944,#20945,#20946,#20947,#20948,#20949,#20950,
#20951,#20952,#20953),.UNSPECIFIED.,.F.,.F.,(4,3,3,3,3,3,4),(2.01694489302844,
2.9499592437288,3.9332789916384,4.916598739548,5.8999184874576,6.8832382353672,
7.59274844815668),.UNSPECIFIED.);
#1511=B_SPLINE_CURVE_WITH_KNOTS('',3,(#20959,#20960,#20961,#20962,#20963,
#20964,#20965,#20966),.UNSPECIFIED.,.F.,.F.,(4,1,1,1,1,4),(40.8407044966673,
41.3585812995958,42.3419010475054,43.325220795415,44.3085405433246,45.2918602912342),
 .UNSPECIFIED.);
#1512=B_SPLINE_CURVE_WITH_KNOTS('',3,(#20969,#20970,#20971,#20972,#20973,
#20974,#20975,#20976,#20977),.UNSPECIFIED.,.F.,.F.,(4,1,1,1,1,1,4),(40.8407044966673,
40.948033320531,41.9313530684406,42.9146728163502,43.8979925642598,44.8813123121694,
45.8143266628698),.UNSPECIFIED.);
#1513=B_SPLINE_CURVE_WITH_KNOTS('',3,(#20982,#20983,#20984,#20985,#20986,
#20987,#20988,#20989,#20990,#20991),.UNSPECIFIED.,.F.,.F.,(4,1,1,1,1,1,
1,4),(34.5575191894877,35.4586628121382,36.4419825600478,37.4253023079574,
38.408622055867,39.3919418037766,40.3752615516862,40.8407044966673),
 .UNSPECIFIED.);
#1514=B_SPLINE_CURVE_WITH_KNOTS('',3,(#20992,#20993,#20994,#20995,#20996,
#20997,#20998,#20999,#21000,#21001),.UNSPECIFIED.,.F.,.F.,(4,1,1,1,1,1,
1,4),(34.5575191894877,35.0481148330734,36.031434580983,37.0147543288926,
37.9980740768022,38.9813938247118,39.9647135726214,40.8407044966673),
 .UNSPECIFIED.);
#1515=B_SPLINE_CURVE_WITH_KNOTS('',3,(#21006,#21007,#21008,#21009,#21010,
#21011,#21012,#21013,#21014,#21015,#21016),.UNSPECIFIED.,.F.,.F.,(4,1,1,
1,1,1,1,1,4),(28.2743338823081,28.575424576771,29.5587443246806,30.5420640725902,
31.5253838204998,32.5087035684094,33.492023316319,34.4753430642286,34.5575191894877),
 .UNSPECIFIED.);
#1516=B_SPLINE_CURVE_WITH_KNOTS('',3,(#21017,#21018,#21019,#21020,#21021,
#21022,#21023,#21024,#21025,#21026),.UNSPECIFIED.,.F.,.F.,(4,1,1,1,1,1,
1,4),(28.2743338823081,29.1481963456159,30.1315160935254,31.114835841435,
32.0981555893446,33.0814753372542,34.0647950851639,34.5575191894877),
 .UNSPECIFIED.);
#1517=B_SPLINE_CURVE_WITH_KNOTS('',3,(#21031,#21032,#21033,#21034,#21035,
#21036,#21037,#21038,#21039,#21040),.UNSPECIFIED.,.F.,.F.,(4,1,1,1,1,1,
1,4),(21.9911485751285,22.6755060893134,23.658825837223,24.6421455851326,
25.6254653330422,26.6087850809518,27.5921048288614,28.2743338823081),
 .UNSPECIFIED.);
#1518=B_SPLINE_CURVE_WITH_KNOTS('',3,(#21041,#21042,#21043,#21044,#21045,
#21046,#21047,#21048,#21049,#21050,#21051),.UNSPECIFIED.,.F.,.F.,(4,1,1,
1,1,1,1,1,4),(21.9911485751285,22.2649581102487,23.2482778581583,24.2315976060679,
25.2149173539775,26.1982371018871,27.1815568497966,28.1648765977063,28.2743338823081),
 .UNSPECIFIED.);
#1519=B_SPLINE_CURVE_WITH_KNOTS('',3,(#21057,#21058,#21059,#21060,#21061),
 .UNSPECIFIED.,.F.,.F.,(4,1,4),(14.3984001269719,15.3817198748815,15.7079632679489),
 .UNSPECIFIED.);
#1520=B_SPLINE_CURVE_WITH_KNOTS('',3,(#21064,#21065,#21066,#21067,#21068),
 .UNSPECIFIED.,.F.,.F.,(4,1,4),(13.8759337553363,14.8089481060366,15.7079632679489),
 .UNSPECIFIED.);
#1521=B_SPLINE_CURVE_WITH_KNOTS('',3,(#21070,#21071,#21072,#21073,#21074,
#21075,#21076,#21077,#21078,#21079,#21080),.UNSPECIFIED.,.F.,.F.,(4,1,1,
1,1,1,1,1,4),(15.7079632679489,15.7922678539462,16.7755876018558,17.7589073497654,
18.742227097675,19.7255468455846,20.7088665934942,21.6921863414038,21.9911485751285),
 .UNSPECIFIED.);
#1522=B_SPLINE_CURVE_WITH_KNOTS('',3,(#21081,#21082,#21083,#21084,#21085,
#21086,#21087,#21088,#21089,#21090),.UNSPECIFIED.,.F.,.F.,(4,1,1,1,1,1,
1,4),(15.7079632679489,16.3650396227911,17.3483593707007,18.3316791186103,
19.3149988665199,20.2983186144295,21.2816383623391,21.9911485751285),
 .UNSPECIFIED.);
#1523=B_SPLINE_CURVE_WITH_KNOTS('',3,(#21239,#21240,#21241,#21242,#21243,
#21244,#21245,#21246,#21247,#21248,#21249,#21250,#21251,#21252,#21253,#21254,
#21255,#21256,#21257,#21258,#21259,#21260,#21261,#21262,#21263,#21264,#21265,
#21266,#21267,#21268,#21269,#21270,#21271,#21272,#21273,#21274,#21275,#21276,
#21277,#21278,#21279,#21280,#21281,#21282,#21283,#21284,#21285,#21286,#21287,
#21288,#21289,#21290,#21291,#21292,#21293,#21294,#21295,#21296,#21297,#21298,
#21299,#21300,#21301,#21302,#21303,#21304,#21305,#21306,#21307,#21308,#21309,
#21310,#21311,#21312,#21313,#21314,#21315,#21316,#21317,#21318,#21319,#21320,
#21321,#21322,#21323,#21324,#21325,#21326),.UNSPECIFIED.,.F.,.F.,(4,3,3,
3,3,3,3,3,3,3,3,3,3,3,3,3,3,3,3,3,3,3,3,3,3,3,3,3,3,4),(0.,0.0297382846428454,
0.0601255889259488,0.0890332382811597,0.114327431466969,0.120650702355347,
0.150403564921709,0.179988720829457,0.207838236564002,0.229395399392172,
0.23393415783729,0.262660470802463,0.291386783767636,0.320322059900051,
0.335078154046361,0.340193241308639,0.344573678198122,0.372678327643481,
0.400795960862634,0.428486852199556,0.439053852931727,0.445278633015735,
0.450309834423539,0.477267903159324,0.497055818929743,0.50468887016549,
0.511949053885254,0.537905662994819,0.556419566241001,0.569248610399422),
 .UNSPECIFIED.);
#1524=B_SPLINE_CURVE_WITH_KNOTS('',3,(#21327,#21328,#21329,#21330,#21331,
#21332,#21333,#21334,#21335,#21336,#21337,#21338,#21339,#21340,#21341,#21342,
#21343,#21344,#21345,#21346,#21347,#21348,#21349,#21350,#21351,#21352,#21353,
#21354,#21355,#21356,#21357,#21358,#21359,#21360,#21361,#21362,#21363,#21364,
#21365,#21366,#21367,#21368,#21369,#21370,#21371,#21372,#21373,#21374,#21375,
#21376,#21377,#21378,#21379,#21380,#21381,#21382,#21383,#21384,#21385,#21386,
#21387,#21388,#21389,#21390,#21391,#21392,#21393,#21394,#21395,#21396,#21397,
#21398,#21399,#21400,#21401,#21402,#21403,#21404,#21405,#21406,#21407,#21408,
#21409,#21410,#21411,#21412,#21413,#21414,#21415,#21416,#21417,#21418,#21419,
#21420),.UNSPECIFIED.,.F.,.F.,(4,3,3,3,3,3,3,3,3,3,3,3,3,3,3,3,3,3,3,3,
3,3,3,3,3,3,3,3,3,3,3,4),(0.,0.0253795104813928,0.0514287956022284,0.0778538073776754,
0.0899945430700518,0.0969018068642677,0.102642146791298,0.129947872947979,
0.157699027910297,0.183981493384174,0.195665040532001,0.201809460807294,
0.206412496951858,0.235040986639171,0.262828889805804,0.290686253909393,
0.306981212992593,0.31132393091396,0.315703998135388,0.34516669827354,0.374337762706802,
0.403793893800065,0.41497713906407,0.422789593408606,0.427299404513114,
0.458325953194986,0.48159586470639,0.493906250475823,0.500072154367986,
0.530578895950629,0.551405599240602,0.566847306048089),.UNSPECIFIED.);
#1525=B_SPLINE_CURVE_WITH_KNOTS('',3,(#21421,#21422,#21423,#21424,#21425,
#21426,#21427,#21428,#21429,#21430,#21431,#21432,#21433,#21434,#21435,#21436,
#21437,#21438,#21439,#21440,#21441,#21442,#21443,#21444,#21445),
 .UNSPECIFIED.,.F.,.F.,(4,3,3,3,3,3,3,3,4),(-10.1321597128207,-9.833197479096,
-8.8498777311864,-7.8665579832768,-6.8832382353672,-5.8999184874576,-4.916598739548,
-3.9332789916384,-3.84897440564114),.UNSPECIFIED.);
#1526=B_SPLINE_CURVE_WITH_KNOTS('',3,(#21594,#21595,#21596,#21597,#21598,
#21599,#21600,#21601,#21602,#21603,#21604,#21605,#21606,#21607,#21608,#21609,
#21610,#21611,#21612,#21613,#21614,#21615,#21616,#21617,#21618,#21619,#21620,
#21621,#21622,#21623,#21624,#21625,#21626,#21627,#21628,#21629,#21630,#21631,
#21632,#21633,#21634,#21635,#21636,#21637,#21638,#21639,#21640,#21641,#21642,
#21643,#21644,#21645,#21646,#21647,#21648,#21649,#21650,#21651,#21652,#21653,
#21654,#21655,#21656,#21657,#21658,#21659,#21660,#21661,#21662,#21663,#21664,
#21665,#21666,#21667,#21668,#21669,#21670,#21671,#21672,#21673,#21674,#21675,
#21676,#21677,#21678,#21679,#21680,#21681,#21682,#21683,#21684,#21685,#21686,
#21687),.UNSPECIFIED.,.F.,.F.,(4,3,3,3,3,3,3,3,3,3,3,3,3,3,3,3,3,3,3,3,
3,3,3,3,3,3,3,3,3,3,3,4),(0.,0.0253795895352918,0.0514289454719094,0.0778539385136474,
0.0899945864079409,0.0969018005134045,0.102642148135923,0.129947928392544,
0.157699108353734,0.183981553716754,0.195665088727664,0.201809360898104,
0.206412522774552,0.235041003890312,0.262828889805813,0.290686211240011,
0.306981172990049,0.311324022663455,0.315704013189775,0.345166711446132,
0.374337752779982,0.403793879145986,0.414977105191051,0.422789478907973,
0.427299173709167,0.458325780092032,0.481595734879181,0.493906100937864,
0.500072114794957,0.530578856744846,0.551405599240626,0.566847306048098),
 .UNSPECIFIED.);
#1527=B_SPLINE_CURVE_WITH_KNOTS('',3,(#21688,#21689,#21690,#21691,#21692,
#21693,#21694,#21695,#21696,#21697,#21698,#21699,#21700,#21701,#21702,#21703,
#21704,#21705,#21706,#21707,#21708,#21709,#21710,#21711,#21712),
 .UNSPECIFIED.,.F.,.F.,(4,3,3,3,3,3,3,3,4),(7.59274844815668,7.8665579832768,
8.84987773118639,9.833197479096,10.8165172270056,11.7998369749152,12.7831567228248,
13.7664764707344,13.8759337553363),.UNSPECIFIED.);
#1528=B_SPLINE_CURVE_WITH_KNOTS('',3,(#21713,#21714,#21715,#21716,#21717,
#21718,#21719,#21720,#21721,#21722,#21723,#21724,#21725,#21726,#21727,#21728,
#21729,#21730,#21731,#21732,#21733,#21734,#21735,#21736,#21737,#21738,#21739,
#21740,#21741,#21742,#21743,#21744,#21745,#21746,#21747,#21748,#21749,#21750,
#21751,#21752,#21753,#21754,#21755,#21756,#21757,#21758,#21759,#21760,#21761,
#21762,#21763,#21764,#21765,#21766,#21767,#21768,#21769,#21770,#21771,#21772,
#21773,#21774,#21775,#21776,#21777,#21778,#21779,#21780,#21781,#21782,#21783,
#21784,#21785,#21786,#21787,#21788,#21789,#21790,#21791,#21792,#21793,#21794,
#21795,#21796,#21797,#21798,#21799,#21800),.UNSPECIFIED.,.F.,.F.,(4,3,3,
3,3,3,3,3,3,3,3,3,3,3,3,3,3,3,3,3,3,3,3,3,3,3,3,3,3,4),(0.,0.0297383502225738,
0.0601256857797807,0.0890333230282637,0.114327505620686,0.120650688809437,
0.150403550371837,0.179988686667598,0.207838210942609,0.229395337968592,
0.23393415684471,0.262660470306177,0.291386783767645,0.32032206170552,0.335078155738989,
0.340193228824031,0.344573672707814,0.372678323504497,0.400795954000531,
0.428486824889168,0.439053762328703,0.445278745781163,0.450309838937034,
0.477267882086698,0.497055803125278,0.504688833353528,0.511949049757023,
0.537905617573998,0.556419566241016,0.569248610399434),.UNSPECIFIED.);
#1957=LINE('',#20747,#2413);
#1958=LINE('',#20768,#2414);
#1959=LINE('',#20819,#2415);
#1960=LINE('',#20870,#2416);
#1961=LINE('',#20918,#2417);
#1962=LINE('',#20957,#2418);
#1963=LINE('',#20981,#2419);
#1964=LINE('',#21005,#2420);
#1965=LINE('',#21030,#2421);
#1966=LINE('',#21055,#2422);
#1967=LINE('',#21804,#2423);
#1968=LINE('',#21806,#2424);
#1969=LINE('',#21808,#2425);
#1970=LINE('',#21810,#2426);
#1971=LINE('',#21812,#2427);
#1972=LINE('',#21813,#2428);
#1973=LINE('',#21818,#2429);
#1974=LINE('',#21819,#2430);
#1975=LINE('',#21820,#2431);
#1976=LINE('',#21823,#2432);
#1977=LINE('',#21824,#2433);
#1978=LINE('',#21827,#2434);
#1979=LINE('',#21828,#2435);
#1980=LINE('',#21831,#2436);
#1981=LINE('',#21832,#2437);
#1982=LINE('',#21835,#2438);
#1983=LINE('',#21836,#2439);
#1984=LINE('',#21838,#2440);
#2413=VECTOR('',#8245,3.);
#2414=VECTOR('',#8250,3.);
#2415=VECTOR('',#8253,3.);
#2416=VECTOR('',#8256,3.);
#2417=VECTOR('',#8259,3.);
#2418=VECTOR('',#8264,3.0735);
#2419=VECTOR('',#8269,3.0735);
#2420=VECTOR('',#8272,3.0735);
#2421=VECTOR('',#8275,3.0735);
#2422=VECTOR('',#8278,3.0735);
#2423=VECTOR('',#8285,10.);
#2424=VECTOR('',#8286,10.);
#2425=VECTOR('',#8287,10.);
#2426=VECTOR('',#8288,10.);
#2427=VECTOR('',#8289,10.);
#2428=VECTOR('',#8290,10.);
#2429=VECTOR('',#8295,10.);
#2430=VECTOR('',#8296,10.);
#2431=VECTOR('',#8297,10.);
#2432=VECTOR('',#8300,10.);
#2433=VECTOR('',#8301,10.);
#2434=VECTOR('',#8304,10.);
#2435=VECTOR('',#8305,10.);
#2436=VECTOR('',#8308,10.);
#2437=VECTOR('',#8309,10.);
#2438=VECTOR('',#8312,10.);
#2439=VECTOR('',#8313,10.);
#2440=VECTOR('',#8316,10.);
#3007=VERTEX_POINT('',#20745);
#3008=VERTEX_POINT('',#20746);
#3009=VERTEX_POINT('',#20748);
#3010=VERTEX_POINT('',#20753);
#3011=VERTEX_POINT('',#20766);
#3012=VERTEX_POINT('',#20767);
#3013=VERTEX_POINT('',#20817);
#3014=VERTEX_POINT('',#20818);
#3015=VERTEX_POINT('',#20868);
#3016=VERTEX_POINT('',#20869);
#3017=VERTEX_POINT('',#20916);
#3018=VERTEX_POINT('',#20917);
#3019=VERTEX_POINT('',#20919);
#3020=VERTEX_POINT('',#20933);
#3021=VERTEX_POINT('',#20955);
#3022=VERTEX_POINT('',#20956);
#3023=VERTEX_POINT('',#20958);
#3024=VERTEX_POINT('',#20967);
#3025=VERTEX_POINT('',#20979);
#3026=VERTEX_POINT('',#20980);
#3027=VERTEX_POINT('',#21003);
#3028=VERTEX_POINT('',#21004);
#3029=VERTEX_POINT('',#21028);
#3030=VERTEX_POINT('',#21029);
#3031=VERTEX_POINT('',#21053);
#3032=VERTEX_POINT('',#21054);
#3033=VERTEX_POINT('',#21056);
#3034=VERTEX_POINT('',#21062);
#3035=VERTEX_POINT('',#21802);
#3036=VERTEX_POINT('',#21803);
#3037=VERTEX_POINT('',#21805);
#3038=VERTEX_POINT('',#21807);
#3039=VERTEX_POINT('',#21809);
#3040=VERTEX_POINT('',#21811);
#3041=VERTEX_POINT('',#21816);
#3042=VERTEX_POINT('',#21817);
#3043=VERTEX_POINT('',#21822);
#3044=VERTEX_POINT('',#21826);
#3045=VERTEX_POINT('',#21830);
#3046=VERTEX_POINT('',#21834);
#3915=EDGE_CURVE('',#3007,#3008,#1957,.T.);
#3916=EDGE_CURVE('',#3008,#3009,#1501,.T.);
#3917=EDGE_CURVE('',#3010,#3009,#1158,.F.);
#3918=EDGE_CURVE('',#3010,#3007,#1502,.T.);
#3919=EDGE_CURVE('',#3011,#3012,#1958,.T.);
#3920=EDGE_CURVE('',#3012,#3008,#1503,.T.);
#3921=EDGE_CURVE('',#3007,#3011,#1504,.T.);
#3922=EDGE_CURVE('',#3013,#3014,#1959,.T.);
#3923=EDGE_CURVE('',#3014,#3012,#1505,.T.);
#3924=EDGE_CURVE('',#3011,#3013,#1506,.T.);
#3925=EDGE_CURVE('',#3015,#3016,#1960,.T.);
#3926=EDGE_CURVE('',#3016,#3014,#1507,.T.);
#3927=EDGE_CURVE('',#3013,#3015,#1508,.T.);
#3928=EDGE_CURVE('',#3017,#3018,#1961,.T.);
#3929=EDGE_CURVE('',#3017,#3019,#1509,.T.);
#3930=EDGE_CURVE('',#3020,#3019,#1159,.T.);
#3931=EDGE_CURVE('',#3020,#3018,#1510,.T.);
#3932=EDGE_CURVE('',#3021,#3022,#1962,.T.);
#3933=EDGE_CURVE('',#3022,#3023,#1511,.T.);
#3934=EDGE_CURVE('',#3024,#3023,#1160,.T.);
#3935=EDGE_CURVE('',#3021,#3024,#1512,.T.);
#3936=EDGE_CURVE('',#3025,#3026,#1963,.T.);
#3937=EDGE_CURVE('',#3026,#3022,#1513,.T.);
#3938=EDGE_CURVE('',#3025,#3021,#1514,.T.);
#3939=EDGE_CURVE('',#3027,#3028,#1964,.T.);
#3940=EDGE_CURVE('',#3028,#3026,#1515,.T.);
#3941=EDGE_CURVE('',#3027,#3025,#1516,.T.);
#3942=EDGE_CURVE('',#3029,#3030,#1965,.T.);
#3943=EDGE_CURVE('',#3030,#3028,#1517,.T.);
#3944=EDGE_CURVE('',#3029,#3027,#1518,.T.);
#3945=EDGE_CURVE('',#3031,#3032,#1966,.T.);
#3946=EDGE_CURVE('',#3033,#3031,#1519,.T.);
#3947=EDGE_CURVE('',#3034,#3033,#1161,.T.);
#3948=EDGE_CURVE('',#3034,#3032,#1520,.T.);
#3949=EDGE_CURVE('',#3032,#3030,#1521,.T.);
#3950=EDGE_CURVE('',#3031,#3029,#1522,.T.);
#3951=EDGE_CURVE('',#3023,#3010,#1523,.T.);
#3952=EDGE_CURVE('',#3019,#3034,#1524,.T.);
#3953=EDGE_CURVE('',#3015,#3017,#1525,.T.);
#3954=EDGE_CURVE('',#3009,#3024,#1526,.T.);
#3955=EDGE_CURVE('',#3018,#3016,#1527,.T.);
#3956=EDGE_CURVE('',#3033,#3020,#1528,.T.);
#3957=EDGE_CURVE('',#3035,#3036,#1967,.T.);
#3958=EDGE_CURVE('',#3036,#3037,#1968,.T.);
#3959=EDGE_CURVE('',#3037,#3038,#1969,.T.);
#3960=EDGE_CURVE('',#3038,#3039,#1970,.T.);
#3961=EDGE_CURVE('',#3039,#3040,#1971,.T.);
#3962=EDGE_CURVE('',#3040,#3035,#1972,.T.);
#3963=EDGE_CURVE('',#3041,#3042,#1973,.T.);
#3964=EDGE_CURVE('',#3042,#3035,#1974,.T.);
#3965=EDGE_CURVE('',#3041,#3040,#1975,.T.);
#3966=EDGE_CURVE('',#3043,#3041,#1976,.T.);
#3967=EDGE_CURVE('',#3043,#3039,#1977,.T.);
#3968=EDGE_CURVE('',#3044,#3043,#1978,.T.);
#3969=EDGE_CURVE('',#3044,#3038,#1979,.T.);
#3970=EDGE_CURVE('',#3045,#3044,#1980,.T.);
#3971=EDGE_CURVE('',#3045,#3037,#1981,.T.);
#3972=EDGE_CURVE('',#3046,#3045,#1982,.T.);
#3973=EDGE_CURVE('',#3046,#3036,#1983,.T.);
#3974=EDGE_CURVE('',#3042,#3046,#1984,.T.);
#5711=ORIENTED_EDGE('',*,*,#3915,.T.);
#5712=ORIENTED_EDGE('',*,*,#3916,.T.);
#5713=ORIENTED_EDGE('',*,*,#3917,.F.);
#5714=ORIENTED_EDGE('',*,*,#3918,.T.);
#5715=ORIENTED_EDGE('',*,*,#3919,.T.);
#5716=ORIENTED_EDGE('',*,*,#3920,.T.);
#5717=ORIENTED_EDGE('',*,*,#3915,.F.);
#5718=ORIENTED_EDGE('',*,*,#3921,.T.);
#5719=ORIENTED_EDGE('',*,*,#3922,.T.);
#5720=ORIENTED_EDGE('',*,*,#3923,.T.);
#5721=ORIENTED_EDGE('',*,*,#3919,.F.);
#5722=ORIENTED_EDGE('',*,*,#3924,.T.);
#5723=ORIENTED_EDGE('',*,*,#3925,.T.);
#5724=ORIENTED_EDGE('',*,*,#3926,.T.);
#5725=ORIENTED_EDGE('',*,*,#3922,.F.);
#5726=ORIENTED_EDGE('',*,*,#3927,.T.);
#5727=ORIENTED_EDGE('',*,*,#3928,.F.);
#5728=ORIENTED_EDGE('',*,*,#3929,.T.);
#5729=ORIENTED_EDGE('',*,*,#3930,.F.);
#5730=ORIENTED_EDGE('',*,*,#3931,.T.);
#5731=ORIENTED_EDGE('',*,*,#3932,.T.);
#5732=ORIENTED_EDGE('',*,*,#3933,.T.);
#5733=ORIENTED_EDGE('',*,*,#3934,.F.);
#5734=ORIENTED_EDGE('',*,*,#3935,.F.);
#5735=ORIENTED_EDGE('',*,*,#3936,.T.);
#5736=ORIENTED_EDGE('',*,*,#3937,.T.);
#5737=ORIENTED_EDGE('',*,*,#3932,.F.);
#5738=ORIENTED_EDGE('',*,*,#3938,.F.);
#5739=ORIENTED_EDGE('',*,*,#3939,.T.);
#5740=ORIENTED_EDGE('',*,*,#3940,.T.);
#5741=ORIENTED_EDGE('',*,*,#3936,.F.);
#5742=ORIENTED_EDGE('',*,*,#3941,.F.);
#5743=ORIENTED_EDGE('',*,*,#3942,.T.);
#5744=ORIENTED_EDGE('',*,*,#3943,.T.);
#5745=ORIENTED_EDGE('',*,*,#3939,.F.);
#5746=ORIENTED_EDGE('',*,*,#3944,.F.);
#5747=ORIENTED_EDGE('',*,*,#3945,.F.);
#5748=ORIENTED_EDGE('',*,*,#3946,.F.);
#5749=ORIENTED_EDGE('',*,*,#3947,.F.);
#5750=ORIENTED_EDGE('',*,*,#3948,.T.);
#5751=ORIENTED_EDGE('',*,*,#3945,.T.);
#5752=ORIENTED_EDGE('',*,*,#3949,.T.);
#5753=ORIENTED_EDGE('',*,*,#3942,.F.);
#5754=ORIENTED_EDGE('',*,*,#3950,.F.);
#5755=ORIENTED_EDGE('',*,*,#3951,.F.);
#5756=ORIENTED_EDGE('',*,*,#3933,.F.);
#5757=ORIENTED_EDGE('',*,*,#3937,.F.);
#5758=ORIENTED_EDGE('',*,*,#3940,.F.);
#5759=ORIENTED_EDGE('',*,*,#3943,.F.);
#5760=ORIENTED_EDGE('',*,*,#3949,.F.);
#5761=ORIENTED_EDGE('',*,*,#3948,.F.);
#5762=ORIENTED_EDGE('',*,*,#3952,.F.);
#5763=ORIENTED_EDGE('',*,*,#3929,.F.);
#5764=ORIENTED_EDGE('',*,*,#3953,.F.);
#5765=ORIENTED_EDGE('',*,*,#3927,.F.);
#5766=ORIENTED_EDGE('',*,*,#3924,.F.);
#5767=ORIENTED_EDGE('',*,*,#3921,.F.);
#5768=ORIENTED_EDGE('',*,*,#3918,.F.);
#5769=ORIENTED_EDGE('',*,*,#3954,.F.);
#5770=ORIENTED_EDGE('',*,*,#3916,.F.);
#5771=ORIENTED_EDGE('',*,*,#3920,.F.);
#5772=ORIENTED_EDGE('',*,*,#3923,.F.);
#5773=ORIENTED_EDGE('',*,*,#3926,.F.);
#5774=ORIENTED_EDGE('',*,*,#3955,.F.);
#5775=ORIENTED_EDGE('',*,*,#3931,.F.);
#5776=ORIENTED_EDGE('',*,*,#3956,.F.);
#5777=ORIENTED_EDGE('',*,*,#3946,.T.);
#5778=ORIENTED_EDGE('',*,*,#3950,.T.);
#5779=ORIENTED_EDGE('',*,*,#3944,.T.);
#5780=ORIENTED_EDGE('',*,*,#3941,.T.);
#5781=ORIENTED_EDGE('',*,*,#3938,.T.);
#5782=ORIENTED_EDGE('',*,*,#3935,.T.);
#5783=ORIENTED_EDGE('',*,*,#3957,.T.);
#5784=ORIENTED_EDGE('',*,*,#3958,.T.);
#5785=ORIENTED_EDGE('',*,*,#3959,.T.);
#5786=ORIENTED_EDGE('',*,*,#3960,.T.);
#5787=ORIENTED_EDGE('',*,*,#3961,.T.);
#5788=ORIENTED_EDGE('',*,*,#3962,.T.);
#5789=ORIENTED_EDGE('',*,*,#3952,.T.);
#5790=ORIENTED_EDGE('',*,*,#3947,.T.);
#5791=ORIENTED_EDGE('',*,*,#3956,.T.);
#5792=ORIENTED_EDGE('',*,*,#3930,.T.);
#5793=ORIENTED_EDGE('',*,*,#3928,.T.);
#5794=ORIENTED_EDGE('',*,*,#3955,.T.);
#5795=ORIENTED_EDGE('',*,*,#3925,.F.);
#5796=ORIENTED_EDGE('',*,*,#3953,.T.);
#5797=ORIENTED_EDGE('',*,*,#3963,.T.);
#5798=ORIENTED_EDGE('',*,*,#3964,.T.);
#5799=ORIENTED_EDGE('',*,*,#3962,.F.);
#5800=ORIENTED_EDGE('',*,*,#3965,.F.);
#5801=ORIENTED_EDGE('',*,*,#3966,.T.);
#5802=ORIENTED_EDGE('',*,*,#3965,.T.);
#5803=ORIENTED_EDGE('',*,*,#3961,.F.);
#5804=ORIENTED_EDGE('',*,*,#3967,.F.);
#5805=ORIENTED_EDGE('',*,*,#3968,.T.);
#5806=ORIENTED_EDGE('',*,*,#3967,.T.);
#5807=ORIENTED_EDGE('',*,*,#3960,.F.);
#5808=ORIENTED_EDGE('',*,*,#3969,.F.);
#5809=ORIENTED_EDGE('',*,*,#3970,.T.);
#5810=ORIENTED_EDGE('',*,*,#3969,.T.);
#5811=ORIENTED_EDGE('',*,*,#3959,.F.);
#5812=ORIENTED_EDGE('',*,*,#3971,.F.);
#5813=ORIENTED_EDGE('',*,*,#3972,.T.);
#5814=ORIENTED_EDGE('',*,*,#3971,.T.);
#5815=ORIENTED_EDGE('',*,*,#3958,.F.);
#5816=ORIENTED_EDGE('',*,*,#3973,.F.);
#5817=ORIENTED_EDGE('',*,*,#3974,.T.);
#5818=ORIENTED_EDGE('',*,*,#3973,.T.);
#5819=ORIENTED_EDGE('',*,*,#3957,.F.);
#5820=ORIENTED_EDGE('',*,*,#3964,.F.);
#5821=ORIENTED_EDGE('',*,*,#3974,.F.);
#5822=ORIENTED_EDGE('',*,*,#3963,.F.);
#5823=ORIENTED_EDGE('',*,*,#3966,.F.);
#5824=ORIENTED_EDGE('',*,*,#3968,.F.);
#5825=ORIENTED_EDGE('',*,*,#3970,.F.);
#5826=ORIENTED_EDGE('',*,*,#3972,.F.);
#5827=ORIENTED_EDGE('',*,*,#3951,.T.);
#5828=ORIENTED_EDGE('',*,*,#3917,.T.);
#5829=ORIENTED_EDGE('',*,*,#3954,.T.);
#5830=ORIENTED_EDGE('',*,*,#3934,.T.);
#6023=CYLINDRICAL_SURFACE('',#6926,2.5175);
#6024=CYLINDRICAL_SURFACE('',#6928,2.5175);
#6025=CYLINDRICAL_SURFACE('',#6929,2.5175);
#6026=CYLINDRICAL_SURFACE('',#6930,2.5175);
#6027=CYLINDRICAL_SURFACE('',#6931,2.5175);
#6028=CYLINDRICAL_SURFACE('',#6933,3.0735);
#6029=CYLINDRICAL_SURFACE('',#6935,3.0735);
#6030=CYLINDRICAL_SURFACE('',#6936,3.0735);
#6031=CYLINDRICAL_SURFACE('',#6937,3.0735);
#6032=CYLINDRICAL_SURFACE('',#6938,3.0735);
#6033=CYLINDRICAL_SURFACE('',#6940,3.0735);
#6034=CYLINDRICAL_SURFACE('',#6942,2.5175);
#6359=ADVANCED_FACE('',(#647),#6023,.F.);
#6360=ADVANCED_FACE('',(#648),#6024,.F.);
#6361=ADVANCED_FACE('',(#649),#6025,.F.);
#6362=ADVANCED_FACE('',(#650),#6026,.F.);
#6363=ADVANCED_FACE('',(#651),#6027,.F.);
#6364=ADVANCED_FACE('',(#652),#6028,.F.);
#6365=ADVANCED_FACE('',(#653),#6029,.F.);
#6366=ADVANCED_FACE('',(#654),#6030,.F.);
#6367=ADVANCED_FACE('',(#655),#6031,.F.);
#6368=ADVANCED_FACE('',(#656),#6032,.F.);
#6369=ADVANCED_FACE('',(#657),#6033,.F.);
#6370=ADVANCED_FACE('',(#658),#141,.F.);
#6371=ADVANCED_FACE('',(#659),#142,.F.);
#6372=ADVANCED_FACE('',(#660,#195),#305,.T.);
#6373=ADVANCED_FACE('',(#661),#6034,.F.);
#6374=ADVANCED_FACE('',(#662),#306,.T.);
#6375=ADVANCED_FACE('',(#663),#307,.T.);
#6376=ADVANCED_FACE('',(#664),#308,.T.);
#6377=ADVANCED_FACE('',(#665),#309,.T.);
#6378=ADVANCED_FACE('',(#666),#310,.T.);
#6379=ADVANCED_FACE('',(#667),#311,.T.);
#6380=ADVANCED_FACE('',(#668,#196),#312,.F.);
#6390=CLOSED_SHELL('',(#6359,#6360,#6361,#6362,#6363,#6364,#6365,#6366,
#6367,#6368,#6369,#6370,#6371,#6372,#6373,#6374,#6375,#6376,#6377,#6378,
#6379,#6380));
#6925=AXIS2_PLACEMENT_3D('',#20743,#8241,#8242);
#6926=AXIS2_PLACEMENT_3D('',#20744,#8243,#8244);
#6927=AXIS2_PLACEMENT_3D('',#20754,#8246,#8247);
#6928=AXIS2_PLACEMENT_3D('',#20765,#8248,#8249);
#6929=AXIS2_PLACEMENT_3D('',#20816,#8251,#8252);
#6930=AXIS2_PLACEMENT_3D('',#20867,#8254,#8255);
#6931=AXIS2_PLACEMENT_3D('',#20915,#8257,#8258);
#6932=AXIS2_PLACEMENT_3D('',#20934,#8260,#8261);
#6933=AXIS2_PLACEMENT_3D('',#20954,#8262,#8263);
#6934=AXIS2_PLACEMENT_3D('',#20968,#8265,#8266);
#6935=AXIS2_PLACEMENT_3D('',#20978,#8267,#8268);
#6936=AXIS2_PLACEMENT_3D('',#21002,#8270,#8271);
#6937=AXIS2_PLACEMENT_3D('',#21027,#8273,#8274);
#6938=AXIS2_PLACEMENT_3D('',#21052,#8276,#8277);
#6939=AXIS2_PLACEMENT_3D('',#21063,#8279,#8280);
#6940=AXIS2_PLACEMENT_3D('',#21069,#8281,#8282);
#6941=AXIS2_PLACEMENT_3D('',#21801,#8283,#8284);
#6942=AXIS2_PLACEMENT_3D('',#21814,#8291,#8292);
#6943=AXIS2_PLACEMENT_3D('',#21815,#8293,#8294);
#6944=AXIS2_PLACEMENT_3D('',#21821,#8298,#8299);
#6945=AXIS2_PLACEMENT_3D('',#21825,#8302,#8303);
#6946=AXIS2_PLACEMENT_3D('',#21829,#8306,#8307);
#6947=AXIS2_PLACEMENT_3D('',#21833,#8310,#8311);
#6948=AXIS2_PLACEMENT_3D('',#21837,#8314,#8315);
#6949=AXIS2_PLACEMENT_3D('',#21839,#8317,#8318);
#8241=DIRECTION('axis',(0.,0.,1.));
#8242=DIRECTION('refdir',(1.,0.,0.));
#8243=DIRECTION('center_axis',(0.,0.,-1.));
#8244=DIRECTION('ref_axis',(-0.346824478021586,0.937930051467088,0.));
#8245=DIRECTION('',(0.,0.,-1.));
#8246=DIRECTION('center_axis',(0.,0.,-1.));
#8247=DIRECTION('ref_axis',(1.,0.,0.));
#8248=DIRECTION('center_axis',(0.,0.,-1.));
#8249=DIRECTION('ref_axis',(1.,0.,0.));
#8250=DIRECTION('',(0.,0.,-1.));
#8251=DIRECTION('center_axis',(0.,0.,-1.));
#8252=DIRECTION('ref_axis',(1.,0.,0.));
#8253=DIRECTION('',(0.,0.,-1.));
#8254=DIRECTION('center_axis',(0.,0.,-1.));
#8255=DIRECTION('ref_axis',(1.,0.,0.));
#8256=DIRECTION('',(0.,0.,-1.));
#8257=DIRECTION('center_axis',(0.,0.,-1.));
#8258=DIRECTION('ref_axis',(0.937996590358642,-0.346644481386278,0.));
#8259=DIRECTION('',(0.,0.,-1.));
#8260=DIRECTION('center_axis',(0.,0.,-1.));
#8261=DIRECTION('ref_axis',(1.,0.,0.));
#8262=DIRECTION('center_axis',(0.,0.,-1.));
#8263=DIRECTION('ref_axis',(0.7932173491397,0.608938615152452,0.));
#8264=DIRECTION('',(1.22464679914735E-16,-9.27389451825078E-31,-1.));
#8265=DIRECTION('center_axis',(0.,0.,1.));
#8266=DIRECTION('ref_axis',(1.,-7.45024487577726E-15,0.));
#8267=DIRECTION('center_axis',(0.,0.,-1.));
#8268=DIRECTION('ref_axis',(1.,-7.45024487577726E-15,0.));
#8269=DIRECTION('',(1.22464679914735E-16,-9.27389451825078E-31,-1.));
#8270=DIRECTION('center_axis',(0.,0.,-1.));
#8271=DIRECTION('ref_axis',(1.,-7.45024487577726E-15,0.));
#8272=DIRECTION('',(1.22464679914735E-16,-9.27389451825078E-31,-1.));
#8273=DIRECTION('center_axis',(0.,0.,-1.));
#8274=DIRECTION('ref_axis',(1.,-7.45024487577726E-15,0.));
#8275=DIRECTION('',(1.22464679914735E-16,-9.27389451825078E-31,-1.));
#8276=DIRECTION('center_axis',(0.,0.,-1.));
#8277=DIRECTION('ref_axis',(-0.609064819364946,-0.793120448489348,0.));
#8278=DIRECTION('',(1.22464679914735E-16,-9.27389451825078E-31,-1.));
#8279=DIRECTION('center_axis',(0.,0.,-1.));
#8280=DIRECTION('ref_axis',(1.,-7.45024487577726E-15,0.));
#8281=DIRECTION('center_axis',(0.,0.,-1.));
#8282=DIRECTION('ref_axis',(1.,-7.45024487577726E-15,0.));
#8283=DIRECTION('center_axis',(0.,0.,1.));
#8284=DIRECTION('ref_axis',(1.,0.,0.));
#8285=DIRECTION('',(0.5,0.866025403784439,0.));
#8286=DIRECTION('',(-0.5,0.866025403784439,0.));
#8287=DIRECTION('',(-1.,1.92296268638356E-16,0.));
#8288=DIRECTION('',(-0.5,-0.866025403784439,0.));
#8289=DIRECTION('',(0.5,-0.866025403784439,0.));
#8290=DIRECTION('',(1.,-1.92296268638356E-16,0.));
#8291=DIRECTION('center_axis',(0.,0.,-1.));
#8292=DIRECTION('ref_axis',(1.,0.,0.));
#8293=DIRECTION('center_axis',(-1.92296268638356E-16,-1.,0.));
#8294=DIRECTION('ref_axis',(1.,-1.92296268638356E-16,0.));
#8295=DIRECTION('',(1.,-1.92296268638356E-16,0.));
#8296=DIRECTION('',(0.,0.,1.));
#8297=DIRECTION('',(0.,0.,1.));
#8298=DIRECTION('center_axis',(-0.866025403784439,-0.5,0.));
#8299=DIRECTION('ref_axis',(0.5,-0.866025403784439,0.));
#8300=DIRECTION('',(0.5,-0.866025403784439,0.));
#8301=DIRECTION('',(0.,0.,1.));
#8302=DIRECTION('center_axis',(-0.866025403784439,0.5,0.));
#8303=DIRECTION('ref_axis',(-0.5,-0.866025403784438,0.));
#8304=DIRECTION('',(-0.5,-0.866025403784439,0.));
#8305=DIRECTION('',(0.,0.,1.));
#8306=DIRECTION('center_axis',(1.92296268638356E-16,1.,0.));
#8307=DIRECTION('ref_axis',(-1.,1.92296268638356E-16,0.));
#8308=DIRECTION('',(-1.,1.92296268638356E-16,0.));
#8309=DIRECTION('',(0.,0.,1.));
#8310=DIRECTION('center_axis',(0.866025403784439,0.5,0.));
#8311=DIRECTION('ref_axis',(-0.5,0.866025403784439,0.));
#8312=DIRECTION('',(-0.5,0.866025403784439,0.));
#8313=DIRECTION('',(0.,0.,1.));
#8314=DIRECTION('center_axis',(0.866025403784439,-0.5,0.));
#8315=DIRECTION('ref_axis',(0.5,0.866025403784439,0.));
#8316=DIRECTION('',(0.5,0.866025403784439,0.));
#8317=DIRECTION('center_axis',(0.,0.,1.));
#8318=DIRECTION('ref_axis',(1.,0.,0.));
#20743=CARTESIAN_POINT('',(0.,0.,0.));
#20744=CARTESIAN_POINT('Origin',(0.,0.,2.5));
#20745=CARTESIAN_POINT('',(-2.513631052301,-0.000262637959241863,0.387416697508025));
#20746=CARTESIAN_POINT('',(-2.5161395146468,-0.00304292125110089,0.112583302491978));
#20747=CARTESIAN_POINT('',(-2.5175,3.08304831685346E-16,2.5));
#20748=CARTESIAN_POINT('',(-1.91346599666505,1.63598720337496,0.));
#20749=CARTESIAN_POINT('Ctrl Pts',(-2.5161395146468,-0.00304292125110089,
0.112583302491978));
#20750=CARTESIAN_POINT('Ctrl Pts',(-2.51095752260429,0.58940711336228,0.0750555349946524));
#20751=CARTESIAN_POINT('Ctrl Pts',(-2.29922182808405,1.18480356030441,0.0375277674973267));
#20752=CARTESIAN_POINT('Ctrl Pts',(-1.91346599666507,1.63598720337494,7.63278329429795E-16));
#20753=CARTESIAN_POINT('',(1.9169334902101,1.63821054532066,9.12403139361656E-16));
#20754=CARTESIAN_POINT('Origin',(0.,0.,0.));
#20755=CARTESIAN_POINT('Ctrl Pts',(1.91694983752521,1.63822102714878,3.46944695195361E-16));
#20756=CARTESIAN_POINT('Ctrl Pts',(1.40805405000164,2.22926133126499,0.0494979486298783));
#20757=CARTESIAN_POINT('Ctrl Pts',(0.602342674674628,2.56946547367296,0.0989958972597568));
#20758=CARTESIAN_POINT('Ctrl Pts',(-0.175477465753492,2.51505986110806,
0.148493845889635));
#20759=CARTESIAN_POINT('Ctrl Pts',(-0.995235386765838,2.4577208574882,0.200660578729532));
#20760=CARTESIAN_POINT('Ctrl Pts',(-1.7840133645033,1.96207254741093,0.252827311569428));
#20761=CARTESIAN_POINT('Ctrl Pts',(-2.1906858971079,1.24828644590423,0.304994044409325));
#20762=CARTESIAN_POINT('Ctrl Pts',(-2.40486472497323,0.872362678473624,
0.332468262108891));
#20763=CARTESIAN_POINT('Ctrl Pts',(-2.51305801188577,0.435933487418771,
0.359942479808458));
#20764=CARTESIAN_POINT('Ctrl Pts',(-2.513631052301,-0.000262637959241863,
0.387416697508025));
#20765=CARTESIAN_POINT('Origin',(0.,0.,2.5));
#20766=CARTESIAN_POINT('',(-2.52068696412108,-0.00113551940461809,1.38741669750803));
#20767=CARTESIAN_POINT('',(-2.52025742113573,0.00144393706437333,1.11258330249198));
#20768=CARTESIAN_POINT('',(-2.5175,3.08304831685346E-16,2.5));
#20769=CARTESIAN_POINT('Ctrl Pts',(-2.52025742113573,0.00144393706437333,
1.11258330249198));
#20770=CARTESIAN_POINT('Ctrl Pts',(-2.52087167159714,0.0912295143008042,
1.10688933154059));
#20771=CARTESIAN_POINT('Ctrl Pts',(-2.51647663371758,0.180953836073687,
1.10119536058921));
#20772=CARTESIAN_POINT('Ctrl Pts',(-2.50686975205229,0.270115985573038,
1.09550138963782));
#20773=CARTESIAN_POINT('Ctrl Pts',(-2.41885391327537,1.08699722224894,1.04333465679793));
#20774=CARTESIAN_POINT('Ctrl Pts',(-1.89336817952545,1.85669104203942,0.991167923958032));
#20775=CARTESIAN_POINT('Ctrl Pts',(-1.16464801024837,2.23624073783096,0.939001191118135));
#20776=CARTESIAN_POINT('Ctrl Pts',(-0.435927840971309,2.6157904336225,0.886834458278239));
#20777=CARTESIAN_POINT('Ctrl Pts',(0.496026763832904,2.60519600541511,0.834667725438342));
#20778=CARTESIAN_POINT('Ctrl Pts',(1.21582156787348,2.20894038730756,0.782500992598446));
#20779=CARTESIAN_POINT('Ctrl Pts',(1.93561637191406,1.81268476920001,0.73033425975855));
#20780=CARTESIAN_POINT('Ctrl Pts',(2.443251375191,1.03076796119231,0.678167526918654));
#20781=CARTESIAN_POINT('Ctrl Pts',(2.51242958730335,0.212179626056957,0.626000794078758));
#20782=CARTESIAN_POINT('Ctrl Pts',(2.58160779941571,-0.606408709078402,
0.573834061238861));
#20783=CARTESIAN_POINT('Ctrl Pts',(2.21232922036347,-1.46166857134141,0.521667328398964));
#20784=CARTESIAN_POINT('Ctrl Pts',(1.56924485086725,-1.97326693907424,0.469500595559067));
#20785=CARTESIAN_POINT('Ctrl Pts',(0.926160481371042,-2.48486530680706,
0.417333862719171));
#20786=CARTESIAN_POINT('Ctrl Pts',(0.00927032143085621,-2.65280218000971,
0.365167129879276));
#20787=CARTESIAN_POINT('Ctrl Pts',(-0.772843960767751,-2.40046341131198,
0.31300039703938));
#20788=CARTESIAN_POINT('Ctrl Pts',(-1.55495824296637,-2.14812464261425,
0.260833664199484));
#20789=CARTESIAN_POINT('Ctrl Pts',(-2.2022966474234,-1.47551023201612,0.208666931359586));
#20790=CARTESIAN_POINT('Ctrl Pts',(-2.42598179621524,-0.686278012308338,
0.15650019851969));
#20791=CARTESIAN_POINT('Ctrl Pts',(-2.48875205155903,-0.464804623376722,
0.141861233177119));
#20792=CARTESIAN_POINT('Ctrl Pts',(-2.51816092457802,-0.234147943006738,
0.127222267834549));
#20793=CARTESIAN_POINT('Ctrl Pts',(-2.5161395146468,-0.00304292125110089,
0.112583302491978));
#20794=CARTESIAN_POINT('Ctrl Pts',(-2.513631052301,-0.000262637959241863,
0.387416697508025));
#20795=CARTESIAN_POINT('Ctrl Pts',(-2.51414607366698,-0.392294889717208,
0.412109212648355));
#20796=CARTESIAN_POINT('Ctrl Pts',(-2.42773023634316,-0.784138881365407,
0.436801727788684));
#20797=CARTESIAN_POINT('Ctrl Pts',(-2.25319678957557,-1.13170015918752,
0.461494242929014));
#20798=CARTESIAN_POINT('Ctrl Pts',(-1.88446806196691,-1.86597676983647,
0.51366097576891));
#20799=CARTESIAN_POINT('Ctrl Pts',(-1.12244351927786,-2.40260609819826,
0.565827708608806));
#20800=CARTESIAN_POINT('Ctrl Pts',(-0.306910970062746,-2.50259594233506,
0.617994441448702));
#20801=CARTESIAN_POINT('Ctrl Pts',(0.508621579152378,-2.60258578647186,
0.670161174288599));
#20802=CARTESIAN_POINT('Ctrl Pts',(1.37766213489358,-2.26593614638367,0.722327907128496));
#20803=CARTESIAN_POINT('Ctrl Pts',(1.91291169988306,-1.64259837236496,0.774494639968393));
#20804=CARTESIAN_POINT('Ctrl Pts',(2.44816126487255,-1.01926059834626,0.826661372808289));
#20805=CARTESIAN_POINT('Ctrl Pts',(2.64961983911033,-0.109234690397042,
0.878828105648185));
#20806=CARTESIAN_POINT('Ctrl Pts',(2.42745590365758,0.681791395088116,0.930994838488081));
#20807=CARTESIAN_POINT('Ctrl Pts',(2.20529196820482,1.47281748057328,0.983161571327977));
#20808=CARTESIAN_POINT('Ctrl Pts',(1.55950552306154,2.14484374359438,1.03532830416787));
#20809=CARTESIAN_POINT('Ctrl Pts',(0.777965481968195,2.39835160459691,1.08749503700777));
#20810=CARTESIAN_POINT('Ctrl Pts',(-0.00357455912515306,2.65185946559944,
1.13966176984767));
#20811=CARTESIAN_POINT('Ctrl Pts',(-0.920868196168557,2.48684892458339,
1.19182850268756));
#20812=CARTESIAN_POINT('Ctrl Pts',(-1.56505239016155,1.97685639415684,1.24399523552746));
#20813=CARTESIAN_POINT('Ctrl Pts',(-2.15540204953033,1.50948398821232,1.29180238952098));
#20814=CARTESIAN_POINT('Ctrl Pts',(-2.51638244467258,0.752380607759215,
1.3396095435145));
#20815=CARTESIAN_POINT('Ctrl Pts',(-2.52068696412108,-0.00113551940461809,
1.38741669750803));
#20816=CARTESIAN_POINT('Origin',(0.,0.,2.5));
#20817=CARTESIAN_POINT('',(-2.51584480336699,0.00196506899055149,2.38741669750802));
#20818=CARTESIAN_POINT('',(-2.51363229639634,1.41266446666228E-5,2.11258330249198));
#20819=CARTESIAN_POINT('',(-2.5175,3.08304831685346E-16,2.5));
#20820=CARTESIAN_POINT('Ctrl Pts',(-2.51363229639634,1.41266446666228E-5,
2.11258330249198));
#20821=CARTESIAN_POINT('Ctrl Pts',(-2.51365314043488,0.413200028375445,
2.08655639524664));
#20822=CARTESIAN_POINT('Ctrl Pts',(-2.41712296010665,0.826376698454607,
2.0605294880013));
#20823=CARTESIAN_POINT('Ctrl Pts',(-2.22398683849327,1.18795070900901,2.03450258075596));
#20824=CARTESIAN_POINT('Ctrl Pts',(-1.83687666966046,1.91266742746658,1.98233584791606));
#20825=CARTESIAN_POINT('Ctrl Pts',(-1.06166440870055,2.43007701911127,1.93016911507617));
#20826=CARTESIAN_POINT('Ctrl Pts',(-0.243891408049745,2.50955308940395,
1.87800238223627));
#20827=CARTESIAN_POINT('Ctrl Pts',(0.573881592601061,2.58902915969663,1.82583564939637));
#20828=CARTESIAN_POINT('Ctrl Pts',(1.43421533294277,2.23057170863728,1.77366891655648));
#20829=CARTESIAN_POINT('Ctrl Pts',(1.95362700805596,1.59395389183621,1.72150218371658));
#20830=CARTESIAN_POINT('Ctrl Pts',(2.47303868316916,0.957336075035145,1.66933545087668));
#20831=CARTESIAN_POINT('Ctrl Pts',(2.65152829305385,0.0425578924923607,
1.61716871803679));
#20832=CARTESIAN_POINT('Ctrl Pts',(2.40953581913432,-0.742620459122797,
1.56500198519689));
#20833=CARTESIAN_POINT('Ctrl Pts',(2.16754334521479,-1.52779881073796,1.51283525235699));
#20834=CARTESIAN_POINT('Ctrl Pts',(1.50506878749103,-2.1833773314255,1.4606685195171));
#20835=CARTESIAN_POINT('Ctrl Pts',(0.717402890595091,-2.41715770945467,
1.4085017866772));
#20836=CARTESIAN_POINT('Ctrl Pts',(-0.0702630063008448,-2.65093808748384,
1.35633505383731));
#20837=CARTESIAN_POINT('Ctrl Pts',(-0.983120242368966,-2.46292032285465,
1.30416832099741));
#20838=CARTESIAN_POINT('Ctrl Pts',(-1.61427588850106,-1.93687711375941,
1.25200158815751));
#20839=CARTESIAN_POINT('Ctrl Pts',(-2.17654123387562,-1.46825123921249,
1.205528826269));
#20840=CARTESIAN_POINT('Ctrl Pts',(-2.51524406302822,-0.731363410840463,
1.15905606438049));
#20841=CARTESIAN_POINT('Ctrl Pts',(-2.52025742113573,0.00144393706437333,
1.11258330249198));
#20842=CARTESIAN_POINT('Ctrl Pts',(-2.52068696412108,-0.00113551940461809,
1.38741669750803));
#20843=CARTESIAN_POINT('Ctrl Pts',(-2.52107949725397,-0.0698493560164091,
1.3917762763544));
#20844=CARTESIAN_POINT('Ctrl Pts',(-2.51850599021738,-0.138533361798365,
1.39613585520078));
#20845=CARTESIAN_POINT('Ctrl Pts',(-2.51286990332195,-0.206965106428379,
1.40049543404715));
#20846=CARTESIAN_POINT('Ctrl Pts',(-2.4454284715468,-1.02581955675002,1.45266216688705));
#20847=CARTESIAN_POINT('Ctrl Pts',(-1.93947085705393,-1.80855393755627,
1.50482889972694));
#20848=CARTESIAN_POINT('Ctrl Pts',(-1.22052386480191,-2.20627819800367,
1.55699563256684));
#20849=CARTESIAN_POINT('Ctrl Pts',(-0.501576872549894,-2.60400245845108,
1.60916236540673));
#20850=CARTESIAN_POINT('Ctrl Pts',(0.430359497461277,-2.61671659853964,
1.66132909824663));
#20851=CARTESIAN_POINT('Ctrl Pts',(1.15988750019281,-2.2387513379105,1.71349583108653));
#20852=CARTESIAN_POINT('Ctrl Pts',(1.88941550292434,-1.86078607728136,1.76566256392642));
#20853=CARTESIAN_POINT('Ctrl Pts',(2.41653513837623,-1.09214141593451,1.81782929676632));
#20854=CARTESIAN_POINT('Ctrl Pts',(2.50628871104416,-0.27543223888268,1.86999602960622));
#20855=CARTESIAN_POINT('Ctrl Pts',(2.59604228371209,0.541276938169144,1.92216276244611));
#20856=CARTESIAN_POINT('Ctrl Pts',(2.24842979359607,1.40605063092595,1.97432949528601));
#20857=CARTESIAN_POINT('Ctrl Pts',(1.61839553463159,1.93342727280644,2.02649622812591));
#20858=CARTESIAN_POINT('Ctrl Pts',(0.9883612756671,2.46080391468694,2.0786629609658));
#20859=CARTESIAN_POINT('Ctrl Pts',(0.0759052478541385,2.6507835056911,2.1308296938057));
#20860=CARTESIAN_POINT('Ctrl Pts',(-0.712256806761665,2.41868475685738,
2.1829964266456));
#20861=CARTESIAN_POINT('Ctrl Pts',(-1.50041886137746,2.18658600802365,2.23516315948549));
#20862=CARTESIAN_POINT('Ctrl Pts',(-2.16428694279611,1.53240891935204,2.28732989232539));
#20863=CARTESIAN_POINT('Ctrl Pts',(-2.40795002197348,0.747744850575128,
2.33949662516528));
#20864=CARTESIAN_POINT('Ctrl Pts',(-2.48255920772454,0.507482158922327,
2.35546998261286));
#20865=CARTESIAN_POINT('Ctrl Pts',(-2.51777110227279,0.254985358855856,
2.37144334006044));
#20866=CARTESIAN_POINT('Ctrl Pts',(-2.51584480336699,0.00196506899055149,
2.38741669750802));
#20867=CARTESIAN_POINT('Origin',(0.,0.,2.5));
#20868=CARTESIAN_POINT('',(-2.51589013302272,-0.00197902614912163,3.38741669750803));
#20869=CARTESIAN_POINT('',(-2.52021651143941,-0.00144364612508765,3.11258330249198));
#20870=CARTESIAN_POINT('',(-2.5175,3.08304831685346E-16,2.5));
#20871=CARTESIAN_POINT('Ctrl Pts',(-2.52021651143941,-0.00144364612508765,
3.11258330249198));
#20872=CARTESIAN_POINT('Ctrl Pts',(-2.51515411267109,0.729619079365268,
3.06622345895268));
#20873=CARTESIAN_POINT('Ctrl Pts',(-2.17829775808437,1.46475479323487,3.01986361541339));
#20874=CARTESIAN_POINT('Ctrl Pts',(-1.61839525002992,1.93342693235859,2.97350377187409));
#20875=CARTESIAN_POINT('Ctrl Pts',(-0.988361101417928,2.4608034807813,2.9213370390342));
#20876=CARTESIAN_POINT('Ctrl Pts',(-0.0759052345218647,2.65078303997177,
2.8691703061943));
#20877=CARTESIAN_POINT('Ctrl Pts',(0.712256681486064,2.41868433245784,2.81700357335441));
#20878=CARTESIAN_POINT('Ctrl Pts',(1.50041859749399,2.18658562494391,2.76483684051451));
#20879=CARTESIAN_POINT('Ctrl Pts',(2.16428656261379,1.53240865072558,2.71267010767461));
#20880=CARTESIAN_POINT('Ctrl Pts',(2.40794959914724,0.747744719274148,2.66050337483472));
#20881=CARTESIAN_POINT('Ctrl Pts',(2.65161263568068,-0.0369192121772903,
2.60833664199482));
#20882=CARTESIAN_POINT('Ctrl Pts',(2.47507074362777,-0.952070100861841,
2.55616990915492));
#20883=CARTESIAN_POINT('Ctrl Pts',(1.95701531533631,-1.58979072079872,2.50400317631503));
#20884=CARTESIAN_POINT('Ctrl Pts',(1.43895988704484,-2.22751134073559,2.45183644347513));
#20885=CARTESIAN_POINT('Ctrl Pts',(0.579390922514817,-2.5878016919248,2.39966971063523));
#20886=CARTESIAN_POINT('Ctrl Pts',(-0.238549412870579,-2.5100671436653,
2.34750297779534));
#20887=CARTESIAN_POINT('Ctrl Pts',(-1.05648974825598,-2.4323325954058,2.29533624495544));
#20888=CARTESIAN_POINT('Ctrl Pts',(-1.83280145449676,-1.91657314769758,
2.24316951211554));
#20889=CARTESIAN_POINT('Ctrl Pts',(-2.22145326926428,-1.19268150120826,
2.19100277927565));
#20890=CARTESIAN_POINT('Ctrl Pts',(-2.41619980794843,-0.829952222250707,
2.16486295368109));
#20891=CARTESIAN_POINT('Ctrl Pts',(-2.51361136192544,-0.414964391838591,
2.13872312808653));
#20892=CARTESIAN_POINT('Ctrl Pts',(-2.51363229639634,1.41266446666228E-5,
2.11258330249198));
#20893=CARTESIAN_POINT('Ctrl Pts',(-2.51584480336699,0.00196506899055149,
2.38741669750802));
#20894=CARTESIAN_POINT('Ctrl Pts',(-2.51148008169565,-0.571343226589796,
2.42361007290034));
#20895=CARTESIAN_POINT('Ctrl Pts',(-2.31644353295754,-1.14733917999922,
2.45980344829266));
#20896=CARTESIAN_POINT('Ctrl Pts',(-1.95701565897371,-1.58979099958587,
2.49599682368498));
#20897=CARTESIAN_POINT('Ctrl Pts',(-1.43896013986049,-2.22751173208773,
2.54816355652487));
#20898=CARTESIAN_POINT('Ctrl Pts',(-0.579391024697962,-2.58780214820923,
2.60033028936477));
#20899=CARTESIAN_POINT('Ctrl Pts',(0.238549454567511,-2.51006758543924,
2.65249702220466));
#20900=CARTESIAN_POINT('Ctrl Pts',(1.05648993383299,-2.43233302266925,2.70466375504456));
#20901=CARTESIAN_POINT('Ctrl Pts',(1.83280177720141,-1.91657348100776,2.75683048788446));
#20902=CARTESIAN_POINT('Ctrl Pts',(2.22145365982248,-1.19268170883292,2.80899722072435));
#20903=CARTESIAN_POINT('Ctrl Pts',(2.61010554244356,-0.468789936658086,
2.86116395356425));
#20904=CARTESIAN_POINT('Ctrl Pts',(2.61109746431729,0.463234066030113,2.91333068640414));
#20905=CARTESIAN_POINT('Ctrl Pts',(2.22398722823793,1.18795091427809,2.96549741924404));
#20906=CARTESIAN_POINT('Ctrl Pts',(1.83687699215856,1.91266776252607,3.01766415208394));
#20907=CARTESIAN_POINT('Ctrl Pts',(1.06166459812611,2.43007745633383,3.06983088492383));
#20908=CARTESIAN_POINT('Ctrl Pts',(0.243891452474371,2.50955353617875,3.12199761776373));
#20909=CARTESIAN_POINT('Ctrl Pts',(-0.573881693177372,2.58902961602367,
3.17416435060363));
#20910=CARTESIAN_POINT('Ctrl Pts',(-1.4342155904484,2.23057208190574,3.22633108344352));
#20911=CARTESIAN_POINT('Ctrl Pts',(-1.95362735417331,1.59395416098643,3.27849781628342));
#20912=CARTESIAN_POINT('Ctrl Pts',(-2.31512049434143,1.1508894724433,3.31480411002495));
#20913=CARTESIAN_POINT('Ctrl Pts',(-2.5114814387863,0.573092447932525,3.35111040376649));
#20914=CARTESIAN_POINT('Ctrl Pts',(-2.51589013302272,-0.00197902614912163,
3.38741669750803));
#20915=CARTESIAN_POINT('Origin',(0.,0.,2.5));
#20916=CARTESIAN_POINT('',(-2.52065797473119,0.00106685237120291,4.38741669750802));
#20917=CARTESIAN_POINT('',(-2.51644348201823,0.00207613456667446,4.11258330249198));
#20918=CARTESIAN_POINT('',(-2.5175,3.08304831685346E-16,2.5));
#20919=CARTESIAN_POINT('',(1.91346599666507,1.63598720337493,5.));
#20920=CARTESIAN_POINT('Ctrl Pts',(-2.52065797473119,0.00106685237120291,
4.38741669750802));
#20921=CARTESIAN_POINT('Ctrl Pts',(-2.51627582008385,-0.750533596725348,
4.43511093315233));
#20922=CARTESIAN_POINT('Ctrl Pts',(-2.1571958584412,-1.50553160271072,4.48280516879663));
#20923=CARTESIAN_POINT('Ctrl Pts',(-1.56924561797524,-1.97326800927033,
4.53049940444093));
#20924=CARTESIAN_POINT('Ctrl Pts',(-0.926160710476491,-2.48486610557827,
4.58266613728083));
#20925=CARTESIAN_POINT('Ctrl Pts',(-0.00926858752154605,-2.65280097461769,
4.63483287012073));
#20926=CARTESIAN_POINT('Ctrl Pts',(0.772845077643461,-2.40046275794039,
4.68699960296062));
#20927=CARTESIAN_POINT('Ctrl Pts',(1.55495874280847,-2.14812454126309,4.73916633580052));
#20928=CARTESIAN_POINT('Ctrl Pts',(2.20229395018354,-1.47551323886906,4.79133306864041));
#20929=CARTESIAN_POINT('Ctrl Pts',(2.42597897401485,-0.686281044499074,
4.84349980148031));
#20930=CARTESIAN_POINT('Ctrl Pts',(2.64966399784617,0.102951149870913,4.89566653432021));
#20931=CARTESIAN_POINT('Ctrl Pts',(2.44969883813372,1.00880423621685,4.9478332671601));
#20932=CARTESIAN_POINT('Ctrl Pts',(1.91346599666506,1.63598720337495,5.));
#20933=CARTESIAN_POINT('',(-1.91693299680257,1.63821185741719,5.));
#20934=CARTESIAN_POINT('Origin',(0.,0.,5.));
#20935=CARTESIAN_POINT('Ctrl Pts',(-1.91694926235926,1.6382222944622,5.));
#20936=CARTESIAN_POINT('Ctrl Pts',(-1.40805335272935,2.22926302987767,4.95050205137012));
#20937=CARTESIAN_POINT('Ctrl Pts',(-0.602342425840394,2.56946465859549,
4.90100410274024));
#20938=CARTESIAN_POINT('Ctrl Pts',(0.175477439781852,2.51505854463557,4.85150615411036));
#20939=CARTESIAN_POINT('Ctrl Pts',(0.995235071171573,2.45771901258696,4.79933942127047));
#20940=CARTESIAN_POINT('Ctrl Pts',(1.78401295214682,1.96207240922004,4.74717268843057));
#20941=CARTESIAN_POINT('Ctrl Pts',(2.19068546260575,1.2482867574395,4.69500595559068));
#20942=CARTESIAN_POINT('Ctrl Pts',(2.59735797306467,0.534501105658956,4.64283922275078));
#20943=CARTESIAN_POINT('Ctrl Pts',(2.62192511300726,-0.397423594535204,
4.59067248991088));
#20944=CARTESIAN_POINT('Ctrl Pts',(2.25319644256834,-1.13170027426973,4.53850575707098));
#20945=CARTESIAN_POINT('Ctrl Pts',(1.88446777212942,-1.86597695400425,4.48633902423109));
#20946=CARTESIAN_POINT('Ctrl Pts',(1.12244329130898,-2.40260561327913,4.43417229139119));
#20947=CARTESIAN_POINT('Ctrl Pts',(0.306910879222839,-2.50259532036743,
4.3820055585513));
#20948=CARTESIAN_POINT('Ctrl Pts',(-0.508621532863308,-2.60258502745572,
4.3298388257114));
#20949=CARTESIAN_POINT('Ctrl Pts',(-1.37766187621516,-2.26593578235743,
4.2776720928715));
#20950=CARTESIAN_POINT('Ctrl Pts',(-1.91291133870635,-1.64259818874412,
4.22550536003161));
#20951=CARTESIAN_POINT('Ctrl Pts',(-2.29911832868587,-1.19283157963813,
4.18786467418506));
#20952=CARTESIAN_POINT('Ctrl Pts',(-2.51154433642508,-0.59380690010991,
4.15022398833852));
#20953=CARTESIAN_POINT('Ctrl Pts',(-2.51644348201823,0.00207613456667446,
4.11258330249198));
#20954=CARTESIAN_POINT('Origin',(0.,0.,7.20842344717746));
#20955=CARTESIAN_POINT('',(-3.07686640868348,0.00176283637231212,0.791576552822548));
#20956=CARTESIAN_POINT('',(-3.06877657964135,-0.000320642608852016,0.708423447177458));
#20957=CARTESIAN_POINT('',(-3.0735,2.32747228194194E-14,7.20842344717746));
#20958=CARTESIAN_POINT('',(0.793799282532827,-2.96922295374571,0.));
#20959=CARTESIAN_POINT('Ctrl Pts',(-3.06877657964135,-0.000320642608851972,
0.708423447177458));
#20960=CARTESIAN_POINT('Ctrl Pts',(-3.06807698094575,0.532211151373012,
0.680949229477891));
#20961=CARTESIAN_POINT('Ctrl Pts',(-2.68518598576605,2.07671369914706,0.601308278938428));
#20962=CARTESIAN_POINT('Ctrl Pts',(-0.25205435815242,3.60563262622145,0.469500595559067));
#20963=CARTESIAN_POINT('Ctrl Pts',(2.8638258713055,2.21030524695087,0.313000397039378));
#20964=CARTESIAN_POINT('Ctrl Pts',(3.4222759216869,-1.16283315864926,0.15650019851969));
#20965=CARTESIAN_POINT('Ctrl Pts',(1.76703113798771,-2.70903678361537,0.0521667328398966));
#20966=CARTESIAN_POINT('Ctrl Pts',(0.793799282532827,-2.96922295374571,
0.));
#20967=CARTESIAN_POINT('',(-0.795749017144049,-2.97385877393435,2.61949253457777E-15));
#20968=CARTESIAN_POINT('Origin',(0.,0.,0.));
#20969=CARTESIAN_POINT('Ctrl Pts',(-3.07686640868348,0.00176283637231189,
0.791576552822548));
#20970=CARTESIAN_POINT('Ctrl Pts',(-3.07761631882972,0.111377919445277,
0.785882581871163));
#20971=CARTESIAN_POINT('Ctrl Pts',(-3.02309142539902,1.22449894749353,0.728021878079882));
#20972=CARTESIAN_POINT('Ctrl Pts',(-1.66998478533906,3.20643252148329,0.617994441448703));
#20973=CARTESIAN_POINT('Ctrl Pts',(1.74335679702331,3.1676297706248,0.461494242929015));
#20974=CARTESIAN_POINT('Ctrl Pts',(3.60260150316633,0.3038109312067,0.304994044409326));
#20975=CARTESIAN_POINT('Ctrl Pts',(2.27315994968988,-2.77521413120327,0.151162630099654));
#20976=CARTESIAN_POINT('Ctrl Pts',(0.124975895037349,-3.21660834551288,
0.0494979486298794));
#20977=CARTESIAN_POINT('Ctrl Pts',(-0.795758164394602,-2.97388052305263,
9.44882193321117E-16));
#20978=CARTESIAN_POINT('Origin',(0.,0.,7.20842344717746));
#20979=CARTESIAN_POINT('',(-3.06877809850016,1.72465709349923E-5,1.79157655282255));
#20980=CARTESIAN_POINT('',(-3.0773908179647,-0.00138630343203515,1.70842344717746));
#20981=CARTESIAN_POINT('',(-3.0735,2.32747228194194E-14,7.20842344717746));
#20982=CARTESIAN_POINT('Ctrl Pts',(-3.0773908179647,-0.00138630343203517,
1.70842344717746));
#20983=CARTESIAN_POINT('Ctrl Pts',(-3.07213562808389,0.918546890942566,
1.66061629318394));
#20984=CARTESIAN_POINT('Ctrl Pts',(-2.15053865242723,2.85146124051564,1.56064240635052));
#20985=CARTESIAN_POINT('Ctrl Pts',(1.11551761111489,3.4389870765969,1.4085017866772));
#20986=CARTESIAN_POINT('Ctrl Pts',(3.48075054753741,0.977649178608381,1.25200158815752));
#20987=CARTESIAN_POINT('Ctrl Pts',(2.74289601575609,-2.35537719050612,1.09550138963782));
#20988=CARTESIAN_POINT('Ctrl Pts',(-0.440018957118456,-3.58837739167123,
0.939001191118136));
#20989=CARTESIAN_POINT('Ctrl Pts',(-2.74101688880118,-1.96797948390379,
0.809975210298013));
#20990=CARTESIAN_POINT('Ctrl Pts',(-3.06940534554735,-0.47893479386132,
0.733115962317788));
#20991=CARTESIAN_POINT('Ctrl Pts',(-3.06877657964135,-0.000320642608851972,
0.708423447177458));
#20992=CARTESIAN_POINT('Ctrl Pts',(-3.06877809850016,1.72465709353392E-5,
1.79157655282255));
#20993=CARTESIAN_POINT('Ctrl Pts',(-3.06880354602845,0.504456916469473,
1.76554964557721));
#20994=CARTESIAN_POINT('Ctrl Pts',(-2.71474447759704,2.01993058914264,1.68735600549197));
#20995=CARTESIAN_POINT('Ctrl Pts',(-0.349716256635896,3.59845088308181,
1.55699563256684));
#20996=CARTESIAN_POINT('Ctrl Pts',(2.8013094644448,2.28557822072128,1.40049543404715));
#20997=CARTESIAN_POINT('Ctrl Pts',(3.45503873870173,-1.0648536490447,1.24399523552746));
#20998=CARTESIAN_POINT('Ctrl Pts',(1.02868455419652,-3.46595066989846,1.08749503700777));
#20999=CARTESIAN_POINT('Ctrl Pts',(-2.1930684252685,-2.80237835053392,0.936688809439468));
#21000=CARTESIAN_POINT('Ctrl Pts',(-3.07074583027496,-0.892887961556386,
0.83804931471106));
#21001=CARTESIAN_POINT('Ctrl Pts',(-3.07686640868348,0.00176283637231189,
0.791576552822548));
#21002=CARTESIAN_POINT('Origin',(0.,0.,7.20842344717746));
#21003=CARTESIAN_POINT('',(-3.0768164639162,-0.00176248117795978,2.79157655282255));
#21004=CARTESIAN_POINT('',(-3.07147924653364,0.00239906238030041,2.70842344717746));
#21005=CARTESIAN_POINT('',(-3.0735,2.32747228194194E-14,7.20842344717746));
#21006=CARTESIAN_POINT('Ctrl Pts',(-3.07147924653364,0.00239906238030076,
2.70842344717746));
#21007=CARTESIAN_POINT('Ctrl Pts',(-3.07383097630006,0.311299900871277,
2.69245008972988));
#21008=CARTESIAN_POINT('Ctrl Pts',(-2.89044774320411,1.62630098606235,2.6243099994424));
#21009=CARTESIAN_POINT('Ctrl Pts',(-1.02130638419203,3.46815705171515,2.50400317631503));
#21010=CARTESIAN_POINT('Ctrl Pts',(2.32062044975012,2.77234500847627,2.34750297779534));
#21011=CARTESIAN_POINT('Ctrl Pts',(3.59377276955738,-0.394942313892847,
2.19100277927565));
#21012=CARTESIAN_POINT('Ctrl Pts',(1.66316438874938,-3.21015109242256,2.03450258075596));
#21013=CARTESIAN_POINT('Ctrl Pts',(-1.7501104075517,-3.16358476523821,1.87800238223627));
#21014=CARTESIAN_POINT('Ctrl Pts',(-3.03713246509983,-1.17251597915295,
1.7693093377101));
#21015=CARTESIAN_POINT('Ctrl Pts',(-3.0778700436187,-0.0852758672160755,
1.71278302602383));
#21016=CARTESIAN_POINT('Ctrl Pts',(-3.0773908179647,-0.00138630343203517,
1.70842344717746));
#21017=CARTESIAN_POINT('Ctrl Pts',(-3.0768164639162,-0.00176248117795985,
2.79157655282255));
#21018=CARTESIAN_POINT('Ctrl Pts',(-3.0706360140197,0.890758387459429,2.74521670928325));
#21019=CARTESIAN_POINT('Ctrl Pts',(-2.19661894703825,2.79816239430364,2.64669013290406));
#21020=CARTESIAN_POINT('Ctrl Pts',(1.02130620401276,3.46815644429995,2.49599682368497));
#21021=CARTESIAN_POINT('Ctrl Pts',(3.45276382958855,1.07219267437738,2.33949662516528));
#21022=CARTESIAN_POINT('Ctrl Pts',(2.8061681927767,-2.27960425476498,2.18299642664559));
#21023=CARTESIAN_POINT('Ctrl Pts',(-0.34205648942751,-3.59919002761108,
2.02649622812591));
#21024=CARTESIAN_POINT('Ctrl Pts',(-2.71249040954675,-2.02434105954679,
1.89602293685156));
#21025=CARTESIAN_POINT('Ctrl Pts',(-3.06875254056717,-0.506610946699481,
1.8177163784171));
#21026=CARTESIAN_POINT('Ctrl Pts',(-3.06877809850016,1.72465709353392E-5,
1.79157655282255));
#21027=CARTESIAN_POINT('Origin',(0.,0.,7.20842344717746));
#21028=CARTESIAN_POINT('',(-3.0722101457728,0.00253465723558749,3.79157655282255));
#21029=CARTESIAN_POINT('',(-3.07153458742615,-0.00241610203352894,3.70842344717746));
#21030=CARTESIAN_POINT('',(-3.0735,2.32747228194194E-14,7.20842344717746));
#21031=CARTESIAN_POINT('Ctrl Pts',(-3.07153458742615,-0.00241610203352869,
3.70842344717746));
#21032=CARTESIAN_POINT('Ctrl Pts',(-3.06615221533653,0.699662219948585,
3.67211715343592));
#21033=CARTESIAN_POINT('Ctrl Pts',(-2.48197069074528,2.41863106906089,3.58364412685449));
#21034=CARTESIAN_POINT('Ctrl Pts',(0.349716325434694,3.59845154159293,3.44300436743317));
#21035=CARTESIAN_POINT('Ctrl Pts',(3.18897983255535,1.70340642470933,3.28650416891347));
#21036=CARTESIAN_POINT('Ctrl Pts',(3.18534685712864,-1.71018933171035,3.13000397039378));
#21037=CARTESIAN_POINT('Ctrl Pts',(0.342056548577105,-3.59919066394061,
2.9735037718741));
#21038=CARTESIAN_POINT('Ctrl Pts',(-2.48484176394183,-2.41428958805909,
2.83297693080198));
#21039=CARTESIAN_POINT('Ctrl Pts',(-3.06615055852694,-0.697526676037249,
2.74461682256977));
#21040=CARTESIAN_POINT('Ctrl Pts',(-3.07147924653364,0.00239906238030076,
2.70842344717746));
#21041=CARTESIAN_POINT('Ctrl Pts',(-3.0722101457728,0.00253465723558725,
3.79157655282255));
#21042=CARTESIAN_POINT('Ctrl Pts',(-3.0745183487722,0.283281367407046,3.77705050582919));
#21043=CARTESIAN_POINT('Ctrl Pts',(-2.91187546114467,1.56963838731655,3.71035772599594));
#21044=CARTESIAN_POINT('Ctrl Pts',(-1.11551737463701,3.43898632522653,3.5914982133228));
#21045=CARTESIAN_POINT('Ctrl Pts',(2.24412684766706,2.83462531411003,3.43499801480311));
#21046=CARTESIAN_POINT('Ctrl Pts',(3.60321095550619,-0.296771509319279,
3.27849781628342));
#21047=CARTESIAN_POINT('Ctrl Pts',(1.75011009124083,-3.16358418358746,3.12199761776373));
#21048=CARTESIAN_POINT('Ctrl Pts',(-1.66316409145381,-3.2101505430571,2.96549741924404));
#21049=CARTESIAN_POINT('Ctrl Pts',(-3.02187071265548,-1.22888761088956,
2.85535706426364));
#21050=CARTESIAN_POINT('Ctrl Pts',(-3.07759060777944,-0.113556859393683,
2.79738344212315));
#21051=CARTESIAN_POINT('Ctrl Pts',(-3.0768164639162,-0.00176248117795985,
2.79157655282255));
#21052=CARTESIAN_POINT('Origin',(0.,0.,7.20842344717746));
#21053=CARTESIAN_POINT('',(-3.07018609065268,-0.00333738419709156,4.79157655282255));
#21054=CARTESIAN_POINT('',(-3.07735542615147,0.00130247100806778,4.70842344717746));
#21055=CARTESIAN_POINT('',(-3.0735,2.32747228194194E-14,7.20842344717746));
#21056=CARTESIAN_POINT('',(-0.793799282532885,-2.96922295374569,5.));
#21057=CARTESIAN_POINT('Ctrl Pts',(-0.793799282532885,-2.96922295374569,
5.));
#21058=CARTESIAN_POINT('Ctrl Pts',(-1.76703113798775,-2.70903678361534,
4.9478332671601));
#21059=CARTESIAN_POINT('Ctrl Pts',(-2.8692411723445,-1.67944397566504,4.87835878476762));
#21060=CARTESIAN_POINT('Ctrl Pts',(-3.07242022864685,-0.338323361726583,
4.80888430237514));
#21061=CARTESIAN_POINT('Ctrl Pts',(-3.07018609065268,-0.00333738419709143,
4.79157655282255));
#21062=CARTESIAN_POINT('',(0.795750420935782,-2.97385779503552,5.));
#21063=CARTESIAN_POINT('Origin',(0.,0.,5.));
#21064=CARTESIAN_POINT('Ctrl Pts',(0.795759619474687,-2.97387964574988,
5.));
#21065=CARTESIAN_POINT('Ctrl Pts',(-0.124974018843371,-3.21660711871812,
4.95050205137012));
#21066=CARTESIAN_POINT('Ctrl Pts',(-2.17865809628841,-2.79463535584754,
4.85330986709594));
#21067=CARTESIAN_POINT('Ctrl Pts',(-3.0720054550259,-0.916291960093509,
4.75611768282176));
#21068=CARTESIAN_POINT('Ctrl Pts',(-3.07735542615147,0.00130247100806802,
4.70842344717746));
#21069=CARTESIAN_POINT('Origin',(0.,0.,7.20842344717746));
#21070=CARTESIAN_POINT('Ctrl Pts',(-3.07735542615147,0.00130247100806811,
4.70842344717746));
#21071=CARTESIAN_POINT('Ctrl Pts',(-3.07785711635642,0.0873493163837036,
4.70395094998186));
#21072=CARTESIAN_POINT('Ctrl Pts',(-3.03598706278426,1.17657551893794,4.64731171994637));
#21073=CARTESIAN_POINT('Ctrl Pts',(-1.74335774093941,3.16762915537798,4.53850575707099));
#21074=CARTESIAN_POINT('Ctrl Pts',(1.66998541626837,3.20643379740356,4.3820055585513));
#21075=CARTESIAN_POINT('Ctrl Pts',(3.59460935228705,0.387380778120988,4.22550536003161));
#21076=CARTESIAN_POINT('Ctrl Pts',(2.31471223100892,-2.77732417593505,4.06900516151192));
#21077=CARTESIAN_POINT('Ctrl Pts',(-1.02868478492208,-3.46595142305511,
3.91250496299223));
#21078=CARTESIAN_POINT('Ctrl Pts',(-2.89215223470734,-1.62188152779685,
3.79231105821408));
#21079=CARTESIAN_POINT('Ctrl Pts',(-3.07388588181438,-0.309119687570202,
3.72428388627582));
#21080=CARTESIAN_POINT('Ctrl Pts',(-3.07153458742615,-0.00241610203352869,
3.70842344717746));
#21081=CARTESIAN_POINT('Ctrl Pts',(-3.07018609065268,-0.00333738419709143,
4.79157655282255));
#21082=CARTESIAN_POINT('Ctrl Pts',(-3.06568638497092,0.671347129621605,
4.75671756953524));
#21083=CARTESIAN_POINT('Ctrl Pts',(-2.51923155566346,2.36462266851063,4.66969185340803));
#21084=CARTESIAN_POINT('Ctrl Pts',(0.252054090990421,3.60562829022214,4.53049940444094));
#21085=CARTESIAN_POINT('Ctrl Pts',(3.14100203598835,1.79029184281612,4.37399920592124));
#21086=CARTESIAN_POINT('Ctrl Pts',(3.23098071080095,-1.62294021205589,4.21749900740156));
#21087=CARTESIAN_POINT('Ctrl Pts',(0.440018754334274,-3.58837598279832,
4.06099880888186));
#21088=CARTESIAN_POINT('Ctrl Pts',(-2.44746347564723,-2.46982179783519,
3.91902465735553));
#21089=CARTESIAN_POINT('Ctrl Pts',(-3.06622900417178,-0.724951542199748,
3.82921723866909));
#21090=CARTESIAN_POINT('Ctrl Pts',(-3.0722101457728,0.00253465723558725,
3.79157655282255));
#21091=CARTESIAN_POINT('Ctrl Pts',(1.91346599666506,1.63598720337495,5.));
#21092=CARTESIAN_POINT('Ctrl Pts',(2.44969883813372,1.00880423621685,4.9478332671601));
#21093=CARTESIAN_POINT('Ctrl Pts',(2.84962915755861,-0.802901936475035,
4.84349980148031));
#21094=CARTESIAN_POINT('Ctrl Pts',(0.907623535433406,-2.82073584365711,
4.68699960296062));
#21095=CARTESIAN_POINT('Ctrl Pts',(-1.84305283343144,-2.31693123653885,
4.53049940444093));
#21096=CARTESIAN_POINT('Ctrl Pts',(-2.95088590955911,0.248852734190564,
4.37399920592124));
#21097=CARTESIAN_POINT('Ctrl Pts',(-1.42798214179762,2.59460107325983,4.21749900740156));
#21098=CARTESIAN_POINT('Ctrl Pts',(1.36788296256894,2.62638590693459,4.06099880888186));
#21099=CARTESIAN_POINT('Ctrl Pts',(2.94434001769405,0.317303110108862,3.90449861036218));
#21100=CARTESIAN_POINT('Ctrl Pts',(1.89597788891003,-2.27490275351114,3.74799841184249));
#21101=CARTESIAN_POINT('Ctrl Pts',(-0.842594418754297,-2.8389564690227,
3.5914982133228));
#21102=CARTESIAN_POINT('Ctrl Pts',(-2.83001837825583,-0.872220375374214,
3.43499801480311));
#21103=CARTESIAN_POINT('Ctrl Pts',(-2.29454948771943,1.8721145477878,3.27849781628342));
#21104=CARTESIAN_POINT('Ctrl Pts',(0.286452204093653,2.9474871501416,3.12199761776373));
#21105=CARTESIAN_POINT('Ctrl Pts',(2.61208938619102,1.39525806871831,2.96549741924404));
#21106=CARTESIAN_POINT('Ctrl Pts',(2.60911362056983,-1.40081393934628,2.80899722072436));
#21107=CARTESIAN_POINT('Ctrl Pts',(0.280178090464571,-2.94809256433073,
2.65249702220466));
#21108=CARTESIAN_POINT('Ctrl Pts',(-2.29852925502302,-1.86722131596623,
2.49599682368498));
#21109=CARTESIAN_POINT('Ctrl Pts',(-2.82815502421476,0.878231830680435,
2.33949662516528));
#21110=CARTESIAN_POINT('Ctrl Pts',(-0.83655077995882,2.84076309669526,2.1829964266456));
#21111=CARTESIAN_POINT('Ctrl Pts',(1.90081730348005,2.27082432368278,2.02649622812591));
#21112=CARTESIAN_POINT('Ctrl Pts',(2.94365477382811,-0.323496754587683,
1.86999602960622));
#21113=CARTESIAN_POINT('Ctrl Pts',(1.36229586747244,-2.6294307386282,1.71349583108653));
#21114=CARTESIAN_POINT('Ctrl Pts',(-1.43351324256106,-2.59128831836252,
1.55699563256684));
#21115=CARTESIAN_POINT('Ctrl Pts',(-2.95138608603967,-0.243085175943775,
1.40049543404715));
#21116=CARTESIAN_POINT('Ctrl Pts',(-1.83816183321196,2.32183838356734,1.24399523552746));
#21117=CARTESIAN_POINT('Ctrl Pts',(0.913719077918246,2.81687000661548,1.08749503700777));
#21118=CARTESIAN_POINT('Ctrl Pts',(2.85107841334811,0.800791217552173,0.930994838488081));
#21119=CARTESIAN_POINT('Ctrl Pts',(2.24670269063477,-1.92928650629548,0.774494639968393));
#21120=CARTESIAN_POINT('Ctrl Pts',(-0.360418976588814,-2.93923542656005,
0.617994441448702));
#21121=CARTESIAN_POINT('Ctrl Pts',(-2.64649260465595,-1.32934744147468,
0.461494242929014));
#21122=CARTESIAN_POINT('Ctrl Pts',(-2.57279134224077,1.46642423733366,0.304994044409324));
#21123=CARTESIAN_POINT('Ctrl Pts',(-0.206457409028375,2.95336916756547,
0.148493845889635));
#21124=CARTESIAN_POINT('Ctrl Pts',(2.34575618383328,1.81045825905282,-0.00800635263005447));
#21125=CARTESIAN_POINT('Ctrl Pts',(2.80318192056183,-0.952475183634134,
-0.164506551149743));
#21126=CARTESIAN_POINT('Ctrl Pts',(1.44737299166554,-2.21896863600185,-0.268840016829536));
#21127=CARTESIAN_POINT('Ctrl Pts',(0.650199997975074,-2.43208680203508,
-0.321006749669432));
#21128=CARTESIAN_POINT('Ctrl Pts',(2.05433155034209,1.75642532122685,5.10700224988981));
#21129=CARTESIAN_POINT('Ctrl Pts',(2.63004078503903,1.08307039382514,5.05483551704991));
#21130=CARTESIAN_POINT('Ctrl Pts',(3.05941317763178,-0.862009977081469,
4.95050205137012));
#21131=CARTESIAN_POINT('Ctrl Pts',(0.974440971474582,-3.02839279553707,
4.79400185285044));
#21132=CARTESIAN_POINT('Ctrl Pts',(-1.97873471034476,-2.48749909718309,
4.63750165433074));
#21133=CARTESIAN_POINT('Ctrl Pts',(-3.16812424993844,0.26717277658844,4.48100145581105));
#21134=CARTESIAN_POINT('Ctrl Pts',(-1.53310734151155,2.78561043396588,4.32450125729137));
#21135=CARTESIAN_POINT('Ctrl Pts',(1.46858378046875,2.81973520375758,4.16800105877167));
#21136=CARTESIAN_POINT('Ctrl Pts',(3.16109646255838,0.34066233277957,4.01150086025199));
#21137=CARTESIAN_POINT('Ctrl Pts',(2.03555600294299,-2.44237656098578,3.8550006617323));
#21138=CARTESIAN_POINT('Ctrl Pts',(-0.904624540810224,-3.0479547870335,
3.69850046321261));
#21139=CARTESIAN_POINT('Ctrl Pts',(-3.03835869183547,-0.936431501320334,
3.54200026469292));
#21140=CARTESIAN_POINT('Ctrl Pts',(-2.46346964861608,2.00993589020025,3.38550006617323));
#21141=CARTESIAN_POINT('Ctrl Pts',(0.307540244540666,3.16447528062537,3.22899986765354));
#21142=CARTESIAN_POINT('Ctrl Pts',(2.8043862016458,1.49797418738198,3.07249966913385));
#21143=CARTESIAN_POINT('Ctrl Pts',(2.80119136608943,-1.50393907013431,2.91599947061416));
#21144=CARTESIAN_POINT('Ctrl Pts',(0.300804243168747,-3.16512526420069,
2.75949927209447));
#21145=CARTESIAN_POINT('Ctrl Pts',(-2.46774239845802,-2.0046824284028,2.60299907357478));
#21146=CARTESIAN_POINT('Ctrl Pts',(-3.03635816138303,0.942885507987068,
2.44649887505509));
#21147=CARTESIAN_POINT('Ctrl Pts',(-0.898135981369886,3.04989441503522,
2.28999867653541));
#21148=CARTESIAN_POINT('Ctrl Pts',(2.04075168557006,2.43799788528061,2.13349847801572));
#21149=CARTESIAN_POINT('Ctrl Pts',(3.16036077240454,-0.347311941022739,
1.97699827949603));
#21150=CARTESIAN_POINT('Ctrl Pts',(1.46258537456475,-2.82300418989299,1.82049808097634));
#21151=CARTESIAN_POINT('Ctrl Pts',(-1.53904563089127,-2.78205380065442,
1.66399788245665));
#21152=CARTESIAN_POINT('Ctrl Pts',(-3.16866124841479,-0.260980622196635,
1.50749768393696));
#21153=CARTESIAN_POINT('Ctrl Pts',(-1.9734836444355,2.49276749859725,1.35099748541727));
#21154=CARTESIAN_POINT('Ctrl Pts',(0.98098525565046,3.02424236327596,1.19449728689758));
#21155=CARTESIAN_POINT('Ctrl Pts',(3.06096912474454,0.859743871237576,1.03799708837789));
#21156=CARTESIAN_POINT('Ctrl Pts',(2.41210046567521,-2.0713167343657,0.881496889858203));
#21157=CARTESIAN_POINT('Ctrl Pts',(-0.386952303432029,-3.15561608159711,
0.724996691338513));
#21158=CARTESIAN_POINT('Ctrl Pts',(-2.84132211649822,-1.42721135110194,
0.568496492818825));
#21159=CARTESIAN_POINT('Ctrl Pts',(-2.76219511400983,1.57437946751671,0.411996294299135));
#21160=CARTESIAN_POINT('Ctrl Pts',(-0.221656392069724,3.1707903204508,0.255496095779446));
#21161=CARTESIAN_POINT('Ctrl Pts',(2.51844607965735,1.94374058835217,0.0989958972597565));
#21162=CARTESIAN_POINT('Ctrl Pts',(3.00954658760352,-1.02259450863918,-0.0575043012599319));
#21163=CARTESIAN_POINT('Ctrl Pts',(1.55392570710626,-2.38232468520636,-0.161837766939725));
#21164=CARTESIAN_POINT('Ctrl Pts',(0.698066426160992,-2.61113218593862,
-0.214004499779622));
#21165=CARTESIAN_POINT('Ctrl Pts',(2.19519710401912,1.87686343907875,5.21400449977962));
#21166=CARTESIAN_POINT('Ctrl Pts',(2.81038273194434,1.15733655143342,5.16183776693973));
#21167=CARTESIAN_POINT('Ctrl Pts',(3.26919719770494,-0.921118017687907,
5.05750430125993));
#21168=CARTESIAN_POINT('Ctrl Pts',(1.04125840751576,-3.23604974741702,4.90100410274025));
#21169=CARTESIAN_POINT('Ctrl Pts',(-2.11441658725808,-2.65806695782732,
4.74450390422055));
#21170=CARTESIAN_POINT('Ctrl Pts',(-3.38536259031776,0.285492818986313,
4.58800370570087));
#21171=CARTESIAN_POINT('Ctrl Pts',(-1.63823254122548,2.97661979467193,4.43150350718118));
#21172=CARTESIAN_POINT('Ctrl Pts',(1.56928459836856,3.01308450058056,4.27500330866148));
#21173=CARTESIAN_POINT('Ctrl Pts',(3.37785290742272,0.364021555450283,4.1185031101418));
#21174=CARTESIAN_POINT('Ctrl Pts',(2.17513411697596,-2.60985036846042,3.96200291162211));
#21175=CARTESIAN_POINT('Ctrl Pts',(-0.966654662866148,-3.25695310504431,
3.80550271310242));
#21176=CARTESIAN_POINT('Ctrl Pts',(-3.24669900541512,-1.00064262726645,
3.64900251458273));
#21177=CARTESIAN_POINT('Ctrl Pts',(-2.63238980951274,2.1477572326127,3.49250231606304));
#21178=CARTESIAN_POINT('Ctrl Pts',(0.328628284987678,3.38146341110915,3.33600211754336));
#21179=CARTESIAN_POINT('Ctrl Pts',(2.99668301710058,1.60069030604565,3.17950191902366));
#21180=CARTESIAN_POINT('Ctrl Pts',(2.99326911160904,-1.60706420092233,3.02300172050398));
#21181=CARTESIAN_POINT('Ctrl Pts',(0.321430395872926,-3.38215796407065,
2.86650152198428));
#21182=CARTESIAN_POINT('Ctrl Pts',(-2.63695554189302,-2.14214354083938,
2.71000132346459));
#21183=CARTESIAN_POINT('Ctrl Pts',(-3.24456129855131,1.0075391852937,2.55350112494491));
#21184=CARTESIAN_POINT('Ctrl Pts',(-0.959721182780959,3.25902573337519,
2.39700092642522));
#21185=CARTESIAN_POINT('Ctrl Pts',(2.18068606766009,2.60517144687844,2.24050072790553));
#21186=CARTESIAN_POINT('Ctrl Pts',(3.37706677098096,-0.371127127457793,
2.08400052938584));
#21187=CARTESIAN_POINT('Ctrl Pts',(1.56287488165706,-3.01657764115777,1.92750033086615));
#21188=CARTESIAN_POINT('Ctrl Pts',(-1.64457801922149,-2.97281928294631,
1.77100013234646));
#21189=CARTESIAN_POINT('Ctrl Pts',(-3.3859364107899,-0.278876068449496,
1.61449993382677));
#21190=CARTESIAN_POINT('Ctrl Pts',(-2.10880545565905,2.66369661362717,1.45799973530708));
#21191=CARTESIAN_POINT('Ctrl Pts',(1.04825143338267,3.23161471993643,1.30149953678739));
#21192=CARTESIAN_POINT('Ctrl Pts',(3.27085983614097,0.918696524922978,1.1449993382677));
#21193=CARTESIAN_POINT('Ctrl Pts',(2.57749824071565,-2.21334696243591,0.988499139748014));
#21194=CARTESIAN_POINT('Ctrl Pts',(-0.413485630275245,-3.37199673663417,
0.831998941228324));
#21195=CARTESIAN_POINT('Ctrl Pts',(-3.03615162834048,-1.52507526072921,
0.675498742708636));
#21196=CARTESIAN_POINT('Ctrl Pts',(-2.9515988857789,1.68233469769977,0.518998544188945));
#21197=CARTESIAN_POINT('Ctrl Pts',(-0.23685537511107,3.38821147333612,0.362498345669257));
#21198=CARTESIAN_POINT('Ctrl Pts',(2.69113597548142,2.07702291765152,0.205998147149567));
#21199=CARTESIAN_POINT('Ctrl Pts',(3.21591125464521,-1.09271383364422,0.049497948629879));
#21200=CARTESIAN_POINT('Ctrl Pts',(1.66047842254699,-2.54568073441086,-0.0548355170499141));
#21201=CARTESIAN_POINT('Ctrl Pts',(0.745932854346909,-2.79017756984216,
-0.107002249889811));
#21202=CARTESIAN_POINT('Ctrl Pts',(2.33606265769615,1.99730155693065,5.32100674966943));
#21203=CARTESIAN_POINT('Ctrl Pts',(2.99072467884965,1.23160270904171,5.26884001682954));
#21204=CARTESIAN_POINT('Ctrl Pts',(3.47898121777811,-0.980226058294341,
5.16450655114975));
#21205=CARTESIAN_POINT('Ctrl Pts',(1.10807584355693,-3.44370669929698,5.00800635263005));
#21206=CARTESIAN_POINT('Ctrl Pts',(-2.25009846417141,-2.82863481847156,
4.85150615411037));
#21207=CARTESIAN_POINT('Ctrl Pts',(-3.60260093069709,0.30381286138419,4.69500595559067));
#21208=CARTESIAN_POINT('Ctrl Pts',(-1.74335774093941,3.16762915537798,4.53850575707099));
#21209=CARTESIAN_POINT('Ctrl Pts',(1.66998541626837,3.20643379740356,4.3820055585513));
#21210=CARTESIAN_POINT('Ctrl Pts',(3.59460935228705,0.387380778120988,4.22550536003161));
#21211=CARTESIAN_POINT('Ctrl Pts',(2.31471223100892,-2.77732417593505,4.06900516151192));
#21212=CARTESIAN_POINT('Ctrl Pts',(-1.02868478492208,-3.46595142305511,
3.91250496299223));
#21213=CARTESIAN_POINT('Ctrl Pts',(-3.45503931899475,-1.06485375321257,
3.75600476447254));
#21214=CARTESIAN_POINT('Ctrl Pts',(-2.8013099704094,2.28557857502515,3.59950456595285));
#21215=CARTESIAN_POINT('Ctrl Pts',(0.349716325434694,3.59845154159293,3.44300436743317));
#21216=CARTESIAN_POINT('Ctrl Pts',(3.18897983255535,1.70340642470933,3.28650416891347));
#21217=CARTESIAN_POINT('Ctrl Pts',(3.18534685712864,-1.71018933171035,3.13000397039378));
#21218=CARTESIAN_POINT('Ctrl Pts',(0.342056548577105,-3.59919066394061,
2.9735037718741));
#21219=CARTESIAN_POINT('Ctrl Pts',(-2.80616868532801,-2.27960465327595,
2.8170035733544));
#21220=CARTESIAN_POINT('Ctrl Pts',(-3.45276443571958,1.07219286260033,2.66050337483472));
#21221=CARTESIAN_POINT('Ctrl Pts',(-1.02130638419203,3.46815705171515,2.50400317631503));
#21222=CARTESIAN_POINT('Ctrl Pts',(2.32062044975012,2.77234500847627,2.34750297779534));
#21223=CARTESIAN_POINT('Ctrl Pts',(3.59377276955738,-0.394942313892847,
2.19100277927565));
#21224=CARTESIAN_POINT('Ctrl Pts',(1.66316438874938,-3.21015109242256,2.03450258075596));
#21225=CARTESIAN_POINT('Ctrl Pts',(-1.7501104075517,-3.16358476523821,1.87800238223627));
#21226=CARTESIAN_POINT('Ctrl Pts',(-3.60321157316502,-0.296771514702359,
1.72150218371658));
#21227=CARTESIAN_POINT('Ctrl Pts',(-2.2441272668826,2.83462572865708,1.56500198519689));
#21228=CARTESIAN_POINT('Ctrl Pts',(1.11551761111489,3.4389870765969,1.4085017866772));
#21229=CARTESIAN_POINT('Ctrl Pts',(3.48075054753741,0.977649178608381,1.25200158815752));
#21230=CARTESIAN_POINT('Ctrl Pts',(2.74289601575609,-2.35537719050612,1.09550138963782));
#21231=CARTESIAN_POINT('Ctrl Pts',(-0.440018957118456,-3.58837739167123,
0.939001191118136));
#21232=CARTESIAN_POINT('Ctrl Pts',(-3.23098114018275,-1.62293917035647,
0.782500992598446));
#21233=CARTESIAN_POINT('Ctrl Pts',(-3.14100265754796,1.79028992788282,0.626000794078757));
#21234=CARTESIAN_POINT('Ctrl Pts',(-0.25205435815242,3.60563262622145,0.469500595559067));
#21235=CARTESIAN_POINT('Ctrl Pts',(2.8638258713055,2.21030524695087,0.313000397039378));
#21236=CARTESIAN_POINT('Ctrl Pts',(3.4222759216869,-1.16283315864926,0.15650019851969));
#21237=CARTESIAN_POINT('Ctrl Pts',(1.76703113798771,-2.70903678361537,0.0521667328398966));
#21238=CARTESIAN_POINT('Ctrl Pts',(0.793799282532827,-2.96922295374571,
0.));
#21239=CARTESIAN_POINT('Ctrl Pts',(0.793799282532827,-2.96922295374571,
0.));
#21240=CARTESIAN_POINT('Ctrl Pts',(0.886893769048896,-2.93516857472777,
6.49317190359092E-17));
#21241=CARTESIAN_POINT('Ctrl Pts',(0.977926242508662,-2.8963539026744,3.5899553935387E-16));
#21242=CARTESIAN_POINT('Ctrl Pts',(1.06668623690149,-2.85310458823344,2.77555756156289E-16));
#21243=CARTESIAN_POINT('Ctrl Pts',(1.1573833631875,-2.8089113842966,1.94338600140189E-16));
#21244=CARTESIAN_POINT('Ctrl Pts',(1.24570840723307,-2.76008724482105,8.94098625496742E-16));
#21245=CARTESIAN_POINT('Ctrl Pts',(1.33140791312673,-2.70693413976456,1.38777878078145E-15));
#21246=CARTESIAN_POINT('Ctrl Pts',(1.41293443628286,-2.65636922920854,1.85742007207992E-15));
#21247=CARTESIAN_POINT('Ctrl Pts',(1.49208510125195,-2.60188577643099,1.19996770961849E-15));
#21248=CARTESIAN_POINT('Ctrl Pts',(1.5686100025003,-2.54371483646266,1.16573417585641E-15));
#21249=CARTESIAN_POINT('Ctrl Pts',(1.63556929109261,-2.49281526399038,1.1357798338146E-15));
#21250=CARTESIAN_POINT('Ctrl Pts',(1.70051795047849,-2.43909179704035,4.6524848618713E-16));
#21251=CARTESIAN_POINT('Ctrl Pts',(1.7632650317936,-2.38268698713509,5.55111512312578E-16));
#21252=CARTESIAN_POINT('Ctrl Pts',(1.77895111395862,-2.36858640326518,5.7757628329248E-16));
#21253=CARTESIAN_POINT('Ctrl Pts',(1.79450367669767,-2.35431414158982,1.61759689860544E-15));
#21254=CARTESIAN_POINT('Ctrl Pts',(1.80989558143071,-2.33989519409729,1.66533453693773E-15));
#21255=CARTESIAN_POINT('Ctrl Pts',(1.88231905248557,-2.27204977506178,1.88995426581157E-15));
#21256=CARTESIAN_POINT('Ctrl Pts',(1.95127638915324,-2.2008843069976,9.33280417709878E-16));
#21257=CARTESIAN_POINT('Ctrl Pts',(2.01652605934852,-2.12668615788006,7.49400541621981E-16));
#21258=CARTESIAN_POINT('Ctrl Pts',(2.08140793958276,-2.05290623822316,5.66557133186095E-16));
#21259=CARTESIAN_POINT('Ctrl Pts',(2.14262432088329,-1.97612693884884,9.5775323130718E-16));
#21260=CARTESIAN_POINT('Ctrl Pts',(2.19989413197892,-1.89660402190249,6.93889390390723E-16));
#21261=CARTESIAN_POINT('Ctrl Pts',(2.25380415733742,-1.82174638945804,4.45505362525734E-16));
#21262=CARTESIAN_POINT('Ctrl Pts',(2.30421707668655,-1.74445688295852,3.26466360005673E-15));
#21263=CARTESIAN_POINT('Ctrl Pts',(2.35085702030783,-1.6649361419825,3.7470027081099E-15));
#21264=CARTESIAN_POINT('Ctrl Pts',(2.38695907926369,-1.60338241236736,4.12036154098178E-15));
#21265=CARTESIAN_POINT('Ctrl Pts',(2.42079974187715,-1.54049148436203,2.76023327184715E-15));
#21266=CARTESIAN_POINT('Ctrl Pts',(2.45223230030139,-1.47635450699168,2.80331313717852E-15));
#21267=CARTESIAN_POINT('Ctrl Pts',(2.45885027647649,-1.46285077043765,2.81238339861069E-15));
#21268=CARTESIAN_POINT('Ctrl Pts',(2.46536173765269,-1.4492909927482,2.25462528933555E-15));
#21269=CARTESIAN_POINT('Ctrl Pts',(2.47175843746063,-1.43569095783397,2.27595720048157E-15));
#21270=CARTESIAN_POINT('Ctrl Pts',(2.51224387039329,-1.34961480639136,2.41096926669652E-15));
#21271=CARTESIAN_POINT('Ctrl Pts',(2.5482055573203,-1.26178852463594,3.62029001511052E-15));
#21272=CARTESIAN_POINT('Ctrl Pts',(2.57938539343216,-1.17245068676435,3.44169137633799E-15));
#21273=CARTESIAN_POINT('Ctrl Pts',(2.61056522954403,-1.08311284889276,3.26309273756545E-15));
#21274=CARTESIAN_POINT('Ctrl Pts',(2.6369636677978,-0.99226274488999,1.94109001754332E-16));
#21275=CARTESIAN_POINT('Ctrl Pts',(2.65826790515113,-0.90012905980095,-3.60822483003176E-16));
#21276=CARTESIAN_POINT('Ctrl Pts',(2.67972711543533,-0.807325168734929,
-9.19790693281215E-16));
#21277=CARTESIAN_POINT('Ctrl Pts',(2.6960170532411,-0.713217781371016,2.19518166871644E-16));
#21278=CARTESIAN_POINT('Ctrl Pts',(2.70721235053312,-0.618215105888531,
0.));
#21279=CARTESIAN_POINT('Ctrl Pts',(2.71292160521868,-0.56976668544991,-1.11947462410922E-16));
#21280=CARTESIAN_POINT('Ctrl Pts',(2.71730508064361,-0.521085594130936,
7.31925815782227E-16));
#21281=CARTESIAN_POINT('Ctrl Pts',(2.72036776812806,-0.472227710003176,
7.49400541621981E-16));
#21282=CARTESIAN_POINT('Ctrl Pts',(2.72142942533794,-0.455291497866967,
7.55458021783632E-16));
#21283=CARTESIAN_POINT('Ctrl Pts',(2.72233234751915,-0.438334056241388,
1.47771822505628E-15));
#21284=CARTESIAN_POINT('Ctrl Pts',(2.72307665503345,-0.421357761541496,
1.52655665885959E-15));
#21285=CARTESIAN_POINT('Ctrl Pts',(2.72371406196817,-0.40681967377542,1.56838071113613E-15));
#21286=CARTESIAN_POINT('Ctrl Pts',(2.72423475300693,-0.392276144899293,
-5.84163957766239E-16));
#21287=CARTESIAN_POINT('Ctrl Pts',(2.72463912967391,-0.377733018449256,
-5.82867087928207E-16));
#21288=CARTESIAN_POINT('Ctrl Pts',(2.7272335888012,-0.284425094826578,-5.74546440218005E-16));
#21289=CARTESIAN_POINT('Ctrl Pts',(2.72504700910767,-0.191075061278942,
2.51838167646803E-15));
#21290=CARTESIAN_POINT('Ctrl Pts',(2.71820565462271,-0.0980605230163078,
1.9151347174784E-15));
#21291=CARTESIAN_POINT('Ctrl Pts',(2.71136113957177,-0.00500301393752514,
1.31160907071961E-15));
#21292=CARTESIAN_POINT('Ctrl Pts',(2.69985717427859,0.0877196672682859,
-3.07238256336187E-16));
#21293=CARTESIAN_POINT('Ctrl Pts',(2.68376968445062,0.179716676654276,-1.04083408558608E-15));
#21294=CARTESIAN_POINT('Ctrl Pts',(2.6679263547778,0.270317445587206,-1.76329611625024E-15));
#21295=CARTESIAN_POINT('Ctrl Pts',(2.64763712143603,0.360215237891958,2.87404250511705E-16));
#21296=CARTESIAN_POINT('Ctrl Pts',(2.62293183221363,0.449011051883673,-1.38777878078145E-17));
#21297=CARTESIAN_POINT('Ctrl Pts',(2.6135041541326,0.482896036662513,-1.28848717445863E-16));
#21298=CARTESIAN_POINT('Ctrl Pts',(2.60343298467484,0.516620214186245,-4.06891175216909E-16));
#21299=CARTESIAN_POINT('Ctrl Pts',(2.592718513,0.550160020505481,-5.82867087928207E-16));
#21300=CARTESIAN_POINT('Ctrl Pts',(2.58640686113371,0.569917558494655,-6.86530500515623E-16));
#21301=CARTESIAN_POINT('Ctrl Pts',(2.57987196088238,0.589611101451674,-5.51406606223906E-16));
#21302=CARTESIAN_POINT('Ctrl Pts',(2.57311372784884,0.609235684372638,-7.21644966006352E-16));
#21303=CARTESIAN_POINT('Ctrl Pts',(2.56765136113167,0.625097325729763,-8.59240746715142E-16));
#21304=CARTESIAN_POINT('Ctrl Pts',(2.56204545311482,0.640906940190805,1.0191622183722E-15));
#21305=CARTESIAN_POINT('Ctrl Pts',(2.55629874325467,0.656655644997032,1.08246744900953E-15));
#21306=CARTESIAN_POINT('Ctrl Pts',(2.52550685343402,0.741039996219253,1.42166809325501E-15));
#21307=CARTESIAN_POINT('Ctrl Pts',(2.49065541114871,0.823737254187918,2.9255481979655E-15));
#21308=CARTESIAN_POINT('Ctrl Pts',(2.45179432548469,0.904376871334311,3.03229663600746E-15));
#21309=CARTESIAN_POINT('Ctrl Pts',(2.42326928916242,0.96356842424157,3.11065273492912E-15));
#21310=CARTESIAN_POINT('Ctrl Pts',(2.39258299461189,1.0216508685957,2.15271533017043E-15));
#21311=CARTESIAN_POINT('Ctrl Pts',(2.35974245541383,1.07846525592557,2.35922392732846E-15));
#21312=CARTESIAN_POINT('Ctrl Pts',(2.3470744452395,1.1003810117054,2.43888318609111E-15));
#21313=CARTESIAN_POINT('Ctrl Pts',(2.33408578165144,1.12210795602091,1.70584578534577E-15));
#21314=CARTESIAN_POINT('Ctrl Pts',(2.32077647825335,1.14363645354687,1.81799020282369E-15));
#21315=CARTESIAN_POINT('Ctrl Pts',(2.30811732205646,1.16411330381573,1.92465646889336E-15));
#21316=CARTESIAN_POINT('Ctrl Pts',(2.29516525813278,1.18441464884107,-2.41812693860714E-17));
#21317=CARTESIAN_POINT('Ctrl Pts',(2.28193698658913,1.20450712017389,0.));
#21318=CARTESIAN_POINT('Ctrl Pts',(2.23464326966583,1.27634172444316,8.6452875223902E-17));
#21319=CARTESIAN_POINT('Ctrl Pts',(2.18378846776941,1.34556635950281,1.71218066021624E-15));
#21320=CARTESIAN_POINT('Ctrl Pts',(2.1293995805356,1.4118263229903,7.73686670285656E-16));
#21321=CARTESIAN_POINT('Ctrl Pts',(2.09060596956493,1.45908713999166,1.04293112238207E-16));
#21322=CARTESIAN_POINT('Ctrl Pts',(2.05001367990221,1.50483902366414,-3.15793211228134E-16));
#21323=CARTESIAN_POINT('Ctrl Pts',(2.00762309288065,1.54893995061572,-2.67147415300428E-16));
#21324=CARTESIAN_POINT('Ctrl Pts',(1.9782489136182,1.57949929468088,-2.39592455248551E-16));
#21325=CARTESIAN_POINT('Ctrl Pts',(1.94801102665337,1.60926561951879,-8.19373708274163E-16));
#21326=CARTESIAN_POINT('Ctrl Pts',(1.91694983752522,1.63822102714876,-8.32667268468867E-16));
#21327=CARTESIAN_POINT('Ctrl Pts',(1.91346599666506,1.63598720337495,5.));
#21328=CARTESIAN_POINT('Ctrl Pts',(1.97511426248036,1.57805297138613,5.));
#21329=CARTESIAN_POINT('Ctrl Pts',(2.0333992327661,1.51697077668011,5.));
#21330=CARTESIAN_POINT('Ctrl Pts',(2.08832045660242,1.45312471107507,5.));
#21331=CARTESIAN_POINT('Ctrl Pts',(2.14469107178614,1.38759372425762,5.));
#21332=CARTESIAN_POINT('Ctrl Pts',(2.19751849836391,1.31915063045882,5.));
#21333=CARTESIAN_POINT('Ctrl Pts',(2.2467768545975,1.24816218982756,5.));
#21334=CARTESIAN_POINT('Ctrl Pts',(2.29674569779122,1.17614983436752,5.));
#21335=CARTESIAN_POINT('Ctrl Pts',(2.34304221736815,1.10151755915666,5.));
#21336=CARTESIAN_POINT('Ctrl Pts',(2.38560686750513,1.02460707565943,5.));
#21337=CARTESIAN_POINT('Ctrl Pts',(2.40516281592033,0.989271240805406,5.));
#21338=CARTESIAN_POINT('Ctrl Pts',(2.42393052938809,0.953453999419588,5.));
#21339=CARTESIAN_POINT('Ctrl Pts',(2.44190157522008,0.917186211225675,5.));
#21340=CARTESIAN_POINT('Ctrl Pts',(2.45212589418763,0.896552273823891,5.));
#21341=CARTESIAN_POINT('Ctrl Pts',(2.46209231213777,0.875772477886718,5.));
#21342=CARTESIAN_POINT('Ctrl Pts',(2.47179901297218,0.854852339979442,5.));
#21343=CARTESIAN_POINT('Ctrl Pts',(2.47986584870041,0.837466482643475,5.));
#21344=CARTESIAN_POINT('Ctrl Pts',(2.48775529546885,0.819978882487774,5.));
#21345=CARTESIAN_POINT('Ctrl Pts',(2.49545397654565,0.802421362463391,5.));
#21346=CARTESIAN_POINT('Ctrl Pts',(2.53207516621785,0.718903515111055,5.));
#21347=CARTESIAN_POINT('Ctrl Pts',(2.56443375074574,0.633702408588491,5.));
#21348=CARTESIAN_POINT('Ctrl Pts',(2.59250161927242,0.547215516795963,5.));
#21349=CARTESIAN_POINT('Ctrl Pts',(2.62102734916793,0.459317794443813,5.));
#21350=CARTESIAN_POINT('Ctrl Pts',(2.64512173324747,0.370091241926015,5.));
#21351=CARTESIAN_POINT('Ctrl Pts',(2.6647162612932,0.279916019321374,5.));
#21352=CARTESIAN_POINT('Ctrl Pts',(2.68327377745922,0.194513189135613,5.));
#21353=CARTESIAN_POINT('Ctrl Pts',(2.69779512543597,0.108258519972062,5.));
#21354=CARTESIAN_POINT('Ctrl Pts',(2.70818462605886,0.0214547457753918,
5.));
#21355=CARTESIAN_POINT('Ctrl Pts',(2.71280315092634,-0.0171328056643356,
5.));
#21356=CARTESIAN_POINT('Ctrl Pts',(2.71660465425308,-0.0558290637111655,
5.));
#21357=CARTESIAN_POINT('Ctrl Pts',(2.71957815680565,-0.0946081258455055,
5.));
#21358=CARTESIAN_POINT('Ctrl Pts',(2.72114193269849,-0.115002176780577,
5.));
#21359=CARTESIAN_POINT('Ctrl Pts',(2.72247667707736,-0.135419134083706,
5.));
#21360=CARTESIAN_POINT('Ctrl Pts',(2.72358060529281,-0.155855252406095,
5.));
#21361=CARTESIAN_POINT('Ctrl Pts',(2.72440760299952,-0.171164783180025,
5.));
#21362=CARTESIAN_POINT('Ctrl Pts',(2.72510503301269,-0.186486473786052,
5.));
#21363=CARTESIAN_POINT('Ctrl Pts',(2.72567165779787,-0.201800403224458,
5.));
#21364=CARTESIAN_POINT('Ctrl Pts',(2.72919576912562,-0.297045075921046,
5.));
#21365=CARTESIAN_POINT('Ctrl Pts',(2.72767362176579,-0.39214594976183,5.));
#21366=CARTESIAN_POINT('Ctrl Pts',(2.72104232884131,-0.48670474660219,5.));
#21367=CARTESIAN_POINT('Ctrl Pts',(2.71460574319996,-0.578487118597797,
5.));
#21368=CARTESIAN_POINT('Ctrl Pts',(2.70335577583384,-0.669759723511558,
5.));
#21369=CARTESIAN_POINT('Ctrl Pts',(2.68719094334706,-0.76017485193479,5.));
#21370=CARTESIAN_POINT('Ctrl Pts',(2.67098570391041,-0.850815989477801,
5.));
#21371=CARTESIAN_POINT('Ctrl Pts',(2.64984154989292,-0.940596245438192,
5.));
#21372=CARTESIAN_POINT('Ctrl Pts',(2.62403295621111,-1.02927270988445,5.));
#21373=CARTESIAN_POINT('Ctrl Pts',(2.60893641023223,-1.08114335185981,5.));
#21374=CARTESIAN_POINT('Ctrl Pts',(2.59224287435959,-1.13263631317645,5.));
#21375=CARTESIAN_POINT('Ctrl Pts',(2.57399925344803,-1.18370190437231,5.));
#21376=CARTESIAN_POINT('Ctrl Pts',(2.56913720383633,-1.19731123330153,5.));
#21377=CARTESIAN_POINT('Ctrl Pts',(2.5641650271584,-1.21089020050661,5.));
#21378=CARTESIAN_POINT('Ctrl Pts',(2.55908354497344,-1.22443784743359,5.));
#21379=CARTESIAN_POINT('Ctrl Pts',(2.55395835978812,-1.23810201013234,5.));
#21380=CARTESIAN_POINT('Ctrl Pts',(2.5487251194683,-1.25172589600239,5.));
#21381=CARTESIAN_POINT('Ctrl Pts',(2.54338628977321,-1.26530561093663,5.));
#21382=CARTESIAN_POINT('Ctrl Pts',(2.507474434899,-1.35665011521995,5.));
#21383=CARTESIAN_POINT('Ctrl Pts',(2.46677381849346,-1.44603954020521,5.));
#21384=CARTESIAN_POINT('Ctrl Pts',(2.42165814194307,-1.53319842974304,5.));
#21385=CARTESIAN_POINT('Ctrl Pts',(2.37698904164233,-1.61949457947533,5.));
#21386=CARTESIAN_POINT('Ctrl Pts',(2.32799127252537,-1.70360490076703,5.));
#21387=CARTESIAN_POINT('Ctrl Pts',(2.27497065048649,-1.78525830139829,5.));
#21388=CARTESIAN_POINT('Ctrl Pts',(2.22143189817264,-1.86770963870577,5.));
#21389=CARTESIAN_POINT('Ctrl Pts',(2.16379086711139,-1.94765663398949,5.));
#21390=CARTESIAN_POINT('Ctrl Pts',(2.10231135200038,-2.02480429723545,5.));
#21391=CARTESIAN_POINT('Ctrl Pts',(2.07897018428145,-2.05409399712484,5.));
#21392=CARTESIAN_POINT('Ctrl Pts',(2.05507524958568,-2.08297997370897,5.));
#21393=CARTESIAN_POINT('Ctrl Pts',(2.03063928040512,-2.11144510112202,5.));
#21394=CARTESIAN_POINT('Ctrl Pts',(2.01356866368511,-2.13133042985048,5.));
#21395=CARTESIAN_POINT('Ctrl Pts',(1.99623399133744,-2.1510103628177,5.));
#21396=CARTESIAN_POINT('Ctrl Pts',(1.97863935752325,-2.17047886391133,5.));
#21397=CARTESIAN_POINT('Ctrl Pts',(1.96848269337448,-2.18171723517703,5.));
#21398=CARTESIAN_POINT('Ctrl Pts',(1.95824201635888,-2.19288219327417,5.));
#21399=CARTESIAN_POINT('Ctrl Pts',(1.94792378478368,-2.20396685638102,5.));
#21400=CARTESIAN_POINT('Ctrl Pts',(1.87693652902952,-2.28022699933091,5.));
#21401=CARTESIAN_POINT('Ctrl Pts',(1.80220735563424,-2.35277244990143,5.));
#21402=CARTESIAN_POINT('Ctrl Pts',(1.7240709087608,-2.42127737465979,5.));
#21403=CARTESIAN_POINT('Ctrl Pts',(1.66546857360572,-2.47265606822857,5.));
#21404=CARTESIAN_POINT('Ctrl Pts',(1.60494837513541,-2.52176172516572,5.));
#21405=CARTESIAN_POINT('Ctrl Pts',(1.5426329601745,-2.56844590489654,5.));
#21406=CARTESIAN_POINT('Ctrl Pts',(1.50966649198766,-2.5931430448721,5.));
#21407=CARTESIAN_POINT('Ctrl Pts',(1.47619735041169,-2.61716230488521,5.));
#21408=CARTESIAN_POINT('Ctrl Pts',(1.44224214591351,-2.64048025951079,5.));
#21409=CARTESIAN_POINT('Ctrl Pts',(1.42523499995595,-2.65215952528491,5.));
#21410=CARTESIAN_POINT('Ctrl Pts',(1.40811304383442,-2.66365787868399,5.));
#21411=CARTESIAN_POINT('Ctrl Pts',(1.39088369966999,-2.6749695061669,5.));
#21412=CARTESIAN_POINT('Ctrl Pts',(1.30563891492228,-2.73093549307415,5.));
#21413=CARTESIAN_POINT('Ctrl Pts',(1.2177306352799,-2.78235921066159,5.));
#21414=CARTESIAN_POINT('Ctrl Pts',(1.12744207813993,-2.82892525415745,5.));
#21415=CARTESIAN_POINT('Ctrl Pts',(1.06580281768531,-2.86071551168622,5.));
#21416=CARTESIAN_POINT('Ctrl Pts',(1.00305327491768,-2.89024121467184,5.));
#21417=CARTESIAN_POINT('Ctrl Pts',(0.939273877630842,-2.91739189131414,
5.));
#21418=CARTESIAN_POINT('Ctrl Pts',(0.891985416295931,-2.93752243153926,
5.));
#21419=CARTESIAN_POINT('Ctrl Pts',(0.84413064869809,-2.95634718738556,5.));
#21420=CARTESIAN_POINT('Ctrl Pts',(0.795759619474682,-2.97387964574988,
5.));
#21421=CARTESIAN_POINT('Ctrl Pts',(-2.51589013302272,-0.00197902614912163,
3.38741669750803));
#21422=CARTESIAN_POINT('Ctrl Pts',(-2.51781607531079,-0.253199548871946,
3.40327713660639));
#21423=CARTESIAN_POINT('Ctrl Pts',(-2.48311008876547,-0.503899930938732,
3.41913757570475));
#21424=CARTESIAN_POINT('Ctrl Pts',(-2.40953623658284,-0.742620570455294,
3.43499801480311));
#21425=CARTESIAN_POINT('Ctrl Pts',(-2.16754372508865,-1.52779907325704,
3.48716474764301));
#21426=CARTESIAN_POINT('Ctrl Pts',(-1.50506907192147,-2.18337777113987,
3.5393314804829));
#21427=CARTESIAN_POINT('Ctrl Pts',(-0.717403027393835,-2.41715816749602,
3.5914982133228));
#21428=CARTESIAN_POINT('Ctrl Pts',(0.0702630171338087,-2.65093856385218,
3.64366494616269));
#21429=CARTESIAN_POINT('Ctrl Pts',(0.983120453021916,-2.46292065868166,
3.69583167900259));
#21430=CARTESIAN_POINT('Ctrl Pts',(1.61427619242997,-1.93687739549307,3.74799841184249));
#21431=CARTESIAN_POINT('Ctrl Pts',(2.24543193183803,-1.41083413230447,3.80016514468238));
#21432=CARTESIAN_POINT('Ctrl Pts',(2.59488597476604,-0.546765511097805,
3.85233187752228));
#21433=CARTESIAN_POINT('Ctrl Pts',(2.50687015370919,0.270115932309816,3.90449861036218));
#21434=CARTESIAN_POINT('Ctrl Pts',(2.41885433265234,1.08699737571744,3.95666534320207));
#21435=CARTESIAN_POINT('Ctrl Pts',(1.89336864761064,1.85669164132601,4.00883207604197));
#21436=CARTESIAN_POINT('Ctrl Pts',(1.16464828769536,2.23624130185117,4.06099880888186));
#21437=CARTESIAN_POINT('Ctrl Pts',(0.435927927780085,2.61579096237633,4.11316554172176));
#21438=CARTESIAN_POINT('Ctrl Pts',(-0.496027107008767,2.60519601781808,
4.16533227456166));
#21439=CARTESIAN_POINT('Ctrl Pts',(-1.21582191903011,2.20894048902741,4.21749900740156));
#21440=CARTESIAN_POINT('Ctrl Pts',(-1.93561673105145,1.81268496023674,4.26966574024145));
#21441=CARTESIAN_POINT('Ctrl Pts',(-2.44325132030528,1.03076884721365,4.32183247308135));
#21442=CARTESIAN_POINT('Ctrl Pts',(-2.51242976891092,0.212180128913875,
4.37399920592124));
#21443=CARTESIAN_POINT('Ctrl Pts',(-2.51836075980379,0.141998702022978,
4.37847170311684));
#21444=CARTESIAN_POINT('Ctrl Pts',(-2.52106890854963,0.0715477156323498,
4.38294420031243));
#21445=CARTESIAN_POINT('Ctrl Pts',(-2.52065797473119,0.00106685237120291,
4.38741669750802));
#21446=CARTESIAN_POINT('Ctrl Pts',(-0.793799282532885,-2.96922295374569,
5.));
#21447=CARTESIAN_POINT('Ctrl Pts',(-1.76703113798775,-2.70903678361534,
4.9478332671601));
#21448=CARTESIAN_POINT('Ctrl Pts',(-3.42227762319113,-1.16284338723151,
4.84349980148031));
#21449=CARTESIAN_POINT('Ctrl Pts',(-2.86382437134345,2.21031103269041,4.68699960296062));
#21450=CARTESIAN_POINT('Ctrl Pts',(0.252054090990421,3.60562829022214,4.53049940444094));
#21451=CARTESIAN_POINT('Ctrl Pts',(3.14100203598835,1.79029184281612,4.37399920592124));
#21452=CARTESIAN_POINT('Ctrl Pts',(3.23098071080095,-1.62294021205589,4.21749900740156));
#21453=CARTESIAN_POINT('Ctrl Pts',(0.440018754334274,-3.58837598279832,
4.06099880888186));
#21454=CARTESIAN_POINT('Ctrl Pts',(-2.74289544065113,-2.35537722830823,
3.90449861036218));
#21455=CARTESIAN_POINT('Ctrl Pts',(-3.48074999950888,0.977649265989379,
3.74799841184248));
#21456=CARTESIAN_POINT('Ctrl Pts',(-1.11551737463701,3.43898632522653,3.5914982133228));
#21457=CARTESIAN_POINT('Ctrl Pts',(2.24412684766706,2.83462531411003,3.43499801480311));
#21458=CARTESIAN_POINT('Ctrl Pts',(3.60321095550619,-0.296771509319279,
3.27849781628342));
#21459=CARTESIAN_POINT('Ctrl Pts',(1.75011009124083,-3.16358418358746,3.12199761776373));
#21460=CARTESIAN_POINT('Ctrl Pts',(-1.66316409145381,-3.2101505430571,2.96549741924404));
#21461=CARTESIAN_POINT('Ctrl Pts',(-3.59377214139091,-0.394942236718185,
2.80899722072435));
#21462=CARTESIAN_POINT('Ctrl Pts',(-2.3206200405613,2.77234451758071,2.65249702220466));
#21463=CARTESIAN_POINT('Ctrl Pts',(1.02130620401276,3.46815644429995,2.49599682368497));
#21464=CARTESIAN_POINT('Ctrl Pts',(3.45276382958855,1.07219267437738,2.33949662516528));
#21465=CARTESIAN_POINT('Ctrl Pts',(2.8061681927767,-2.27960425476498,2.18299642664559));
#21466=CARTESIAN_POINT('Ctrl Pts',(-0.34205648942751,-3.59919002761108,
2.02649622812591));
#21467=CARTESIAN_POINT('Ctrl Pts',(-3.18534629574052,-1.71018903949051,
1.86999602960622));
#21468=CARTESIAN_POINT('Ctrl Pts',(-3.18897927637007,1.7034061403768,1.71349583108653));
#21469=CARTESIAN_POINT('Ctrl Pts',(-0.349716256635896,3.59845088308181,
1.55699563256684));
#21470=CARTESIAN_POINT('Ctrl Pts',(2.8013094644448,2.28557822072128,1.40049543404715));
#21471=CARTESIAN_POINT('Ctrl Pts',(3.45503873870173,-1.0648536490447,1.24399523552746));
#21472=CARTESIAN_POINT('Ctrl Pts',(1.02868455419652,-3.46595066989846,1.08749503700777));
#21473=CARTESIAN_POINT('Ctrl Pts',(-2.31471172988138,-2.77732393751975,
0.930994838488083));
#21474=CARTESIAN_POINT('Ctrl Pts',(-3.5946088997546,0.387381135037168,0.774494639968393));
#21475=CARTESIAN_POINT('Ctrl Pts',(-1.66998478533906,3.20643252148329,0.617994441448703));
#21476=CARTESIAN_POINT('Ctrl Pts',(1.74335679702331,3.1676297706248,0.461494242929015));
#21477=CARTESIAN_POINT('Ctrl Pts',(3.60260150316633,0.3038109312067,0.304994044409326));
#21478=CARTESIAN_POINT('Ctrl Pts',(2.25009578791265,-2.82863139649778,0.148493845889636));
#21479=CARTESIAN_POINT('Ctrl Pts',(-1.10807133015233,-3.44371061769541,
-0.00800635263005217));
#21480=CARTESIAN_POINT('Ctrl Pts',(-3.47898841388462,-0.980218592702346,
-0.164506551149742));
#21481=CARTESIAN_POINT('Ctrl Pts',(-2.99072467884965,1.23160270904172,-0.268840016829535));
#21482=CARTESIAN_POINT('Ctrl Pts',(-2.33606265769614,1.99730155693066,-0.321006749669431));
#21483=CARTESIAN_POINT('Ctrl Pts',(-0.745932854346964,-2.79017756984215,
5.10700224988981));
#21484=CARTESIAN_POINT('Ctrl Pts',(-1.66047842254703,-2.54568073441083,
5.05483551704991));
#21485=CARTESIAN_POINT('Ctrl Pts',(-3.21591285354802,-1.09272344543869,
4.95050205137012));
#21486=CARTESIAN_POINT('Ctrl Pts',(-2.69113456596771,2.07702835450855,4.79400185285043));
#21487=CARTESIAN_POINT('Ctrl Pts',(0.236855124059054,3.38820739879938,4.63750165433075));
#21488=CARTESIAN_POINT('Ctrl Pts',(2.95159830169959,1.68233649716179,4.48100145581105));
#21489=CARTESIAN_POINT('Ctrl Pts',(3.03615122485059,-1.52507623961371,4.32450125729137));
#21490=CARTESIAN_POINT('Ctrl Pts',(0.413485439719026,-3.37199541271688,
4.16800105877167));
#21491=CARTESIAN_POINT('Ctrl Pts',(-2.57749770028975,-2.21334699795853,
4.01150086025199));
#21492=CARTESIAN_POINT('Ctrl Pts',(-3.2708593211588,0.918696607034865,3.85500066173229));
#21493=CARTESIAN_POINT('Ctrl Pts',(-1.04825121116451,3.231614013874,3.69850046321261));
#21494=CARTESIAN_POINT('Ctrl Pts',(2.10880506172238,2.66369622407748,3.54200026469292));
#21495=CARTESIAN_POINT('Ctrl Pts',(3.38593583037616,-0.278876063391019,
3.38550006617323));
#21496=CARTESIAN_POINT('Ctrl Pts',(1.64457772198429,-2.97281873636934,3.22899986765354));
#21497=CARTESIAN_POINT('Ctrl Pts',(-1.56287460228854,-3.01657712491928,
3.07249966913385));
#21498=CARTESIAN_POINT('Ctrl Pts',(-3.37706618069319,-0.371127054936794,
2.91599947061416));
#21499=CARTESIAN_POINT('Ctrl Pts',(-2.18068568314553,2.60517098558408,2.75949927209447));
#21500=CARTESIAN_POINT('Ctrl Pts',(0.95972101346657,3.25902516258738,2.60299907357479));
#21501=CARTESIAN_POINT('Ctrl Pts',(3.24456072897023,1.00753900842068,2.44649887505509));
#21502=CARTESIAN_POINT('Ctrl Pts',(2.63695507904276,-2.14214316635878,2.28999867653541));
#21503=CARTESIAN_POINT('Ctrl Pts',(-0.321430340290076,-3.38215736611206,
2.13349847801571));
#21504=CARTESIAN_POINT('Ctrl Pts',(-2.99326858407285,-1.60706392632346,
1.97699827949603));
#21505=CARTESIAN_POINT('Ctrl Pts',(-2.9966824944535,1.60069003885849,1.82049808097634));
#21506=CARTESIAN_POINT('Ctrl Pts',(-0.32862822033748,3.38146279230653,1.66399788245665));
#21507=CARTESIAN_POINT('Ctrl Pts',(2.63238933405802,2.1477568996735,1.50749768393696));
#21508=CARTESIAN_POINT('Ctrl Pts',(3.246698460114,-1.00064252937995,1.35099748541727));
#21509=CARTESIAN_POINT('Ctrl Pts',(0.96665444605344,-3.25695239730331,1.19449728689758));
#21510=CARTESIAN_POINT('Ctrl Pts',(-2.17513364606662,-2.60985014442166,
1.03799708837789));
#21511=CARTESIAN_POINT('Ctrl Pts',(-3.37785248217816,0.364021890844269,
0.881496889858204));
#21512=CARTESIAN_POINT('Ctrl Pts',(-1.56928400548455,3.01308330159882,0.724996691338513));
#21513=CARTESIAN_POINT('Ctrl Pts',(1.63823165422791,2.9766203728191,0.568496492818826));
#21514=CARTESIAN_POINT('Ctrl Pts',(3.38536312826686,0.285491005199331,0.411996294299136));
#21515=CARTESIAN_POINT('Ctrl Pts',(2.11441407237884,-2.65806374219999,0.255496095779446));
#21516=CARTESIAN_POINT('Ctrl Pts',(-1.04125416627134,-3.2360534295344,0.0989958972597585));
#21517=CARTESIAN_POINT('Ctrl Pts',(-3.26920395988323,-0.921111002274222,
-0.0575043012599318));
#21518=CARTESIAN_POINT('Ctrl Pts',(-2.81038273194434,1.15733655143344,-0.161837766939724));
#21519=CARTESIAN_POINT('Ctrl Pts',(-2.19519710401911,1.87686343907876,-0.214004499779621));
#21520=CARTESIAN_POINT('Ctrl Pts',(-0.698066426161043,-2.61113218593861,
5.21400449977962));
#21521=CARTESIAN_POINT('Ctrl Pts',(-1.55392570710631,-2.38232468520633,
5.16183776693972));
#21522=CARTESIAN_POINT('Ctrl Pts',(-3.00954808390491,-1.02260350364586,
5.05750430125993));
#21523=CARTESIAN_POINT('Ctrl Pts',(-2.51844476059198,1.94374567632669,4.90100410274025));
#21524=CARTESIAN_POINT('Ctrl Pts',(0.221656157127689,3.17078650737663,4.74450390422055));
#21525=CARTESIAN_POINT('Ctrl Pts',(2.76219456741083,1.57438115150745,4.58800370570087));
#21526=CARTESIAN_POINT('Ctrl Pts',(2.84132173890023,-1.42721226717154,4.43150350718117));
#21527=CARTESIAN_POINT('Ctrl Pts',(0.386952125103784,-3.15561484263544,
4.27500330866149));
#21528=CARTESIAN_POINT('Ctrl Pts',(-2.41209995992838,-2.07131676760884,
4.11850311014179));
#21529=CARTESIAN_POINT('Ctrl Pts',(-3.06096864280872,0.859743948080353,
3.96200291162211));
#21530=CARTESIAN_POINT('Ctrl Pts',(-0.98098504769201,3.02424170252148,3.80550271310242));
#21531=CARTESIAN_POINT('Ctrl Pts',(1.9734832757777,2.49276713404493,3.64900251458273));
#21532=CARTESIAN_POINT('Ctrl Pts',(3.16866070524613,-0.260980617462761,
3.49250231606304));
#21533=CARTESIAN_POINT('Ctrl Pts',(1.53904535272775,-2.78205328915123,3.33600211754335));
#21534=CARTESIAN_POINT('Ctrl Pts',(-1.46258511312328,-2.82300370678147,
3.17950191902366));
#21535=CARTESIAN_POINT('Ctrl Pts',(-3.16036021999547,-0.347311873155402,
3.02300172050397));
#21536=CARTESIAN_POINT('Ctrl Pts',(-2.04075132572976,2.43799745358745,2.86650152198428));
#21537=CARTESIAN_POINT('Ctrl Pts',(0.898135822920388,3.04989388087481,2.7100013234646));
#21538=CARTESIAN_POINT('Ctrl Pts',(3.03635762835191,0.942885342463967,2.5535011249449));
#21539=CARTESIAN_POINT('Ctrl Pts',(2.46774196530881,-2.00468207795258,2.39700092642522));
#21540=CARTESIAN_POINT('Ctrl Pts',(-0.300804191152645,-3.16512470461303,
2.24050072790553));
#21541=CARTESIAN_POINT('Ctrl Pts',(-2.80119087240519,-1.50393881315642,
2.08400052938584));
#21542=CARTESIAN_POINT('Ctrl Pts',(-2.80438571253693,1.49797393734019,1.92750033086615));
#21543=CARTESIAN_POINT('Ctrl Pts',(-0.307540184039062,3.16447470153125,
1.77100013234646));
#21544=CARTESIAN_POINT('Ctrl Pts',(2.46346920367124,2.00993557862573,1.61449993382677));
#21545=CARTESIAN_POINT('Ctrl Pts',(3.03835818152627,-0.936431409715195,
1.45799973530708));
#21546=CARTESIAN_POINT('Ctrl Pts',(0.904624337910361,-3.04795412470817,
1.30149953678739));
#21547=CARTESIAN_POINT('Ctrl Pts',(-2.03555556225185,-2.44237635132356,
1.1449993382677));
#21548=CARTESIAN_POINT('Ctrl Pts',(-3.16109606460172,0.340662646651362,
0.988499139748014));
#21549=CARTESIAN_POINT('Ctrl Pts',(-1.46858322563004,2.81973408171437,0.831998941228325));
#21550=CARTESIAN_POINT('Ctrl Pts',(1.53310651143252,2.78561097501341,0.675498742708636));
#21551=CARTESIAN_POINT('Ctrl Pts',(3.1681247533674,0.267171079191969,0.518998544188947));
#21552=CARTESIAN_POINT('Ctrl Pts',(1.97873235684504,-2.4874960879022,0.362498345669256));
#21553=CARTESIAN_POINT('Ctrl Pts',(-0.974437002390344,-3.02839624137338,
0.205998147149569));
#21554=CARTESIAN_POINT('Ctrl Pts',(-3.05941950588183,-0.862003411846101,
0.0494979486298786));
#21555=CARTESIAN_POINT('Ctrl Pts',(-2.63004078503903,1.08307039382515,-0.0548355170499138));
#21556=CARTESIAN_POINT('Ctrl Pts',(-2.05433155034208,1.75642532122686,-0.10700224988981));
#21557=CARTESIAN_POINT('Ctrl Pts',(-0.650199997975122,-2.43208680203507,
5.32100674966943));
#21558=CARTESIAN_POINT('Ctrl Pts',(-1.44737299166558,-2.21896863600183,
5.26884001682953));
#21559=CARTESIAN_POINT('Ctrl Pts',(-2.80318331426181,-0.952483561853041,
5.16450655114974));
#21560=CARTESIAN_POINT('Ctrl Pts',(-2.34575495521625,1.81046299814482,5.00800635263005));
#21561=CARTESIAN_POINT('Ctrl Pts',(0.206457190196319,2.95336561595388,4.85150615411036));
#21562=CARTESIAN_POINT('Ctrl Pts',(2.57279083312207,1.46642580585312,4.69500595559068));
#21563=CARTESIAN_POINT('Ctrl Pts',(2.64649225294986,-1.32934829472936,4.53850575707098));
#21564=CARTESIAN_POINT('Ctrl Pts',(0.360418810488541,-2.93923427255401,
4.3820055585513));
#21565=CARTESIAN_POINT('Ctrl Pts',(-2.24670221956701,-1.92928653725914,
4.22550536003161));
#21566=CARTESIAN_POINT('Ctrl Pts',(-2.85107796445863,0.800791289125838,
4.06900516151192));
#21567=CARTESIAN_POINT('Ctrl Pts',(-0.913718884219513,2.81686939116895,
3.91250496299223));
#21568=CARTESIAN_POINT('Ctrl Pts',(1.83816148983303,2.32183804401237,3.75600476447254));
#21569=CARTESIAN_POINT('Ctrl Pts',(2.9513855801161,-0.243085171534501,3.59950456595285));
#21570=CARTESIAN_POINT('Ctrl Pts',(1.43351298347121,-2.59128784193311,3.44300436743316));
#21571=CARTESIAN_POINT('Ctrl Pts',(-1.36229562395802,-2.62943028864365,
3.28650416891347));
#21572=CARTESIAN_POINT('Ctrl Pts',(-2.94365425929774,-0.323496691374012,
3.13000397039378));
#21573=CARTESIAN_POINT('Ctrl Pts',(-1.90081696831399,2.27082392159083,2.97350377187409));
#21574=CARTESIAN_POINT('Ctrl Pts',(0.836550632374203,2.84076259916223,2.81700357335441));
#21575=CARTESIAN_POINT('Ctrl Pts',(2.82815452773359,0.878231676507261,2.66050337483472));
#21576=CARTESIAN_POINT('Ctrl Pts',(2.29852885157487,-1.86722098954639,2.50400317631502));
#21577=CARTESIAN_POINT('Ctrl Pts',(-0.280178042015212,-2.948092043114,2.34750297779534));
#21578=CARTESIAN_POINT('Ctrl Pts',(-2.60911316073752,-1.40081369998938,
2.19100277927565));
#21579=CARTESIAN_POINT('Ctrl Pts',(-2.61208893062035,1.39525783582189,2.03450258075596));
#21580=CARTESIAN_POINT('Ctrl Pts',(-0.286452147740644,2.94748661075597,
1.87800238223627));
#21581=CARTESIAN_POINT('Ctrl Pts',(2.29454907328446,1.87211425757795,1.72150218371658));
#21582=CARTESIAN_POINT('Ctrl Pts',(2.83001790293854,-0.872220290050442,
1.56500198519689));
#21583=CARTESIAN_POINT('Ctrl Pts',(0.842594229767281,-2.83895585211302,
1.4085017866772));
#21584=CARTESIAN_POINT('Ctrl Pts',(-1.89597747843709,-2.27490255822547,
1.25200158815751));
#21585=CARTESIAN_POINT('Ctrl Pts',(-2.94433964702528,0.317303402458459,
1.09550138963782));
#21586=CARTESIAN_POINT('Ctrl Pts',(-1.36788244577553,2.6263848618299,0.939001191118136));
#21587=CARTESIAN_POINT('Ctrl Pts',(1.42798136863712,2.59460157720772,0.782500992598445));
#21588=CARTESIAN_POINT('Ctrl Pts',(2.95088637846794,0.248851153184599,0.626000794078758));
#21589=CARTESIAN_POINT('Ctrl Pts',(1.84305064131124,-2.31692843360441,0.469500595559067));
#21590=CARTESIAN_POINT('Ctrl Pts',(-0.907619838509351,-2.82073905321236,
0.31300039703938));
#21591=CARTESIAN_POINT('Ctrl Pts',(-2.84963505188044,-0.802895821417979,
0.156500198519689));
#21592=CARTESIAN_POINT('Ctrl Pts',(-2.44969883813372,1.00880423621686,0.0521667328398966));
#21593=CARTESIAN_POINT('Ctrl Pts',(-1.91346599666505,1.63598720337496,0.));
#21594=CARTESIAN_POINT('Ctrl Pts',(-1.91346599666505,1.63598720337496,0.));
#21595=CARTESIAN_POINT('Ctrl Pts',(-1.97511445450674,1.57805279092849,-2.16023702375061E-17));
#21596=CARTESIAN_POINT('Ctrl Pts',(-2.03339962644492,1.51697042789119,-3.49443898869507E-17));
#21597=CARTESIAN_POINT('Ctrl Pts',(-2.08832105501608,1.45312420295415,-1.11022302462516E-16));
#21598=CARTESIAN_POINT('Ctrl Pts',(-2.1446918579957,1.38759307857242,-1.89107908253736E-16));
#21599=CARTESIAN_POINT('Ctrl Pts',(-2.19751947843796,1.31914985899599,-1.96056269520747E-15));
#21600=CARTESIAN_POINT('Ctrl Pts',(-2.2467780277058,1.24816130047737,-2.16493489801906E-15));
#21601=CARTESIAN_POINT('Ctrl Pts',(-2.29674689545117,1.17614907224947,-2.37225419030257E-15));
#21602=CARTESIAN_POINT('Ctrl Pts',(-2.34304346389473,1.10151695033136,8.04059381600243E-19));
#21603=CARTESIAN_POINT('Ctrl Pts',(-2.38560818063646,1.02460663863002,2.77555756156289E-16));
#21604=CARTESIAN_POINT('Ctrl Pts',(-2.40516403209366,0.989271113192736,
4.04706022549276E-16));
#21605=CARTESIAN_POINT('Ctrl Pts',(-2.42393166263322,0.953454191414296,
1.85001145283656E-16));
#21606=CARTESIAN_POINT('Ctrl Pts',(-2.44190263911885,0.917186731710372,
2.77555756156289E-16));
#21607=CARTESIAN_POINT('Ctrl Pts',(-2.45212691902149,0.896552980413291,
3.30213120022811E-16));
#21608=CARTESIAN_POINT('Ctrl Pts',(-2.46209330228438,0.875773373445736,
1.0101923078241E-15));
#21609=CARTESIAN_POINT('Ctrl Pts',(-2.47179997273461,0.85485342713836,9.99200722162641E-16));
#21610=CARTESIAN_POINT('Ctrl Pts',(-2.47986685205683,0.837467580657393,
9.90065994086157E-16));
#21611=CARTESIAN_POINT('Ctrl Pts',(-2.48775634234785,0.819979991507439,
-1.29538532938285E-15));
#21612=CARTESIAN_POINT('Ctrl Pts',(-2.49545506671926,0.802422482605945,
-1.22124532708767E-15));
#21613=CARTESIAN_POINT('Ctrl Pts',(-2.53207648579799,0.718904634655909,
-8.68574941246235E-16));
#21614=CARTESIAN_POINT('Ctrl Pts',(-2.56443528935485,0.633703528135737,
-2.73580965033665E-16));
#21615=CARTESIAN_POINT('Ctrl Pts',(-2.59250335927894,0.547216632073775,
-2.22044604925031E-16));
#21616=CARTESIAN_POINT('Ctrl Pts',(-2.62102926303655,0.45931900035097,-1.696676067042E-16));
#21617=CARTESIAN_POINT('Ctrl Pts',(-2.64512381235207,0.370092536921413,
8.62583150244892E-16));
#21618=CARTESIAN_POINT('Ctrl Pts',(-2.6647184895653,0.279917395525893,9.71445146547012E-16));
#21619=CARTESIAN_POINT('Ctrl Pts',(-2.68327611608723,0.194514784532604,
1.07454560836236E-15));
#21620=CARTESIAN_POINT('Ctrl Pts',(-2.69779757345701,0.108260330337431,
1.58880599429527E-15));
#21621=CARTESIAN_POINT('Ctrl Pts',(-2.70818717658801,0.0214567600039818,
1.52655665885959E-15));
#21622=CARTESIAN_POINT('Ctrl Pts',(-2.71280574576047,-0.0171306902524466,
1.49888448909292E-15));
#21623=CARTESIAN_POINT('Ctrl Pts',(-2.71660729247955,-0.0558268492504973,
1.27797020542778E-15));
#21624=CARTESIAN_POINT('Ctrl Pts',(-2.71958083700161,-0.0946058150986653,
1.2490009027033E-15));
#21625=CARTESIAN_POINT('Ctrl Pts',(-2.72114459889708,-0.114999345005228,
1.23376619160252E-15));
#21626=CARTESIAN_POINT('Ctrl Pts',(-2.72247933944975,-0.135415780987334,
2.7744501595987E-15));
#21627=CARTESIAN_POINT('Ctrl Pts',(-2.72358327406089,-0.155851378047186,
2.83106871279415E-15));
#21628=CARTESIAN_POINT('Ctrl Pts',(-2.72441031908349,-0.171161305520925,
2.87348616409501E-15));
#21629=CARTESIAN_POINT('Ctrl Pts',(-2.72510778883702,-0.186483394270956,
-3.27116286657501E-16));
#21630=CARTESIAN_POINT('Ctrl Pts',(-2.72567444563692,-0.201797722043239,
-3.05311331771918E-16));
#21631=CARTESIAN_POINT('Ctrl Pts',(-2.72919865876058,-0.297042242048632,
-1.69699603154258E-16));
#21632=CARTESIAN_POINT('Ctrl Pts',(-2.7276765940473,-0.392142984842673,
1.65684655347014E-15));
#21633=CARTESIAN_POINT('Ctrl Pts',(-2.72104535728848,-0.486701680153984,
1.80411241501588E-15));
#21634=CARTESIAN_POINT('Ctrl Pts',(-2.71460882823241,-0.578483924102048,
1.94705422681979E-15));
#21635=CARTESIAN_POINT('Ctrl Pts',(-2.70335889560743,-0.669756429091281,
-1.44907627993903E-16));
#21636=CARTESIAN_POINT('Ctrl Pts',(-2.68719406942169,-0.760171493259568,
-2.4980018054066E-16));
#21637=CARTESIAN_POINT('Ctrl Pts',(-2.67098885106311,-0.850812483822458,
-3.27199259771174E-16));
#21638=CARTESIAN_POINT('Ctrl Pts',(-2.64984469854827,-0.940592630196976,
2.00672834831372E-15));
#21639=CARTESIAN_POINT('Ctrl Pts',(-2.62403609171522,-1.02926901742914,
1.97064586870965E-15));
#21640=CARTESIAN_POINT('Ctrl Pts',(-2.60893951244934,-1.08113970217868,
1.94953965336933E-15));
#21641=CARTESIAN_POINT('Ctrl Pts',(-2.59224593286086,-1.13263271607333,
1.51263892527377E-15));
#21642=CARTESIAN_POINT('Ctrl Pts',(-2.57400225902127,-1.18369836845093,
1.4432899320127E-15));
#21643=CARTESIAN_POINT('Ctrl Pts',(-2.56914004859136,-1.19730812434678,
1.42480739382975E-15));
#21644=CARTESIAN_POINT('Ctrl Pts',(-2.56416770379457,-1.21088751729747,
1.46101747209947E-15));
#21645=CARTESIAN_POINT('Ctrl Pts',(-2.55908604628673,-1.22443558863974,
1.41553435639707E-15));
#21646=CARTESIAN_POINT('Ctrl Pts',(-2.55396092950485,-1.23809952559165,
1.36966226068444E-15));
#21647=CARTESIAN_POINT('Ctrl Pts',(-2.54872776110117,-1.25172318692358,
7.2111001976691E-16));
#21648=CARTESIAN_POINT('Ctrl Pts',(-2.54338900633193,-1.26530267978209,
8.04911692853238E-16));
#21649=CARTESIAN_POINT('Ctrl Pts',(-2.50747702892334,-1.35664728387668,
1.36861688643376E-15));
#21650=CARTESIAN_POINT('Ctrl Pts',(-2.46677626545746,-1.44603683426546,
3.98698161417476E-15));
#21651=CARTESIAN_POINT('Ctrl Pts',(-2.42166042457756,-1.53319586749654,
3.8441472227646E-15));
#21652=CARTESIAN_POINT('Ctrl Pts',(-2.37699119409271,-1.6194920966769,3.70272677649499E-15));
#21653=CARTESIAN_POINT('Ctrl Pts',(-2.32799328414659,-1.70360251853944,
2.71566994649136E-15));
#21654=CARTESIAN_POINT('Ctrl Pts',(-2.27497251664925,-1.78525603476489,
3.10862446895044E-15));
#21655=CARTESIAN_POINT('Ctrl Pts',(-2.22143358365231,-1.86770754085407,
3.50541928807182E-15));
#21656=CARTESIAN_POINT('Ctrl Pts',(-2.16379236200239,-1.94765471708648,
2.12393071997628E-15));
#21657=CARTESIAN_POINT('Ctrl Pts',(-2.10231265300888,-2.02480256688325,
2.24820162486594E-15));
#21658=CARTESIAN_POINT('Ctrl Pts',(-2.07897144804811,-2.05409229196278,
2.29538195003625E-15));
#21659=CARTESIAN_POINT('Ctrl Pts',(-2.05507647736,-2.082978295804,3.52826900319682E-15));
#21660=CARTESIAN_POINT('Ctrl Pts',(-2.03064047373774,-2.11144345226609,
3.52495810318487E-15));
#21661=CARTESIAN_POINT('Ctrl Pts',(-2.01356997979656,-2.13132863023677,
3.52264517593754E-15));
#21662=CARTESIAN_POINT('Ctrl Pts',(-1.99623543552702,-2.15100841685411,
2.17794287054721E-15));
#21663=CARTESIAN_POINT('Ctrl Pts',(-1.97864093508987,-2.17047677606985,
2.02615701994091E-15));
#21664=CARTESIAN_POINT('Ctrl Pts',(-1.96848450504363,-2.18171489159328,
1.93853859740034E-15));
#21665=CARTESIAN_POINT('Ctrl Pts',(-1.95824406587573,-2.19287959838895,
2.78311917693584E-15));
#21666=CARTESIAN_POINT('Ctrl Pts',(-1.94792607632517,-2.20396401413293,
2.80331313717852E-15));
#21667=CARTESIAN_POINT('Ctrl Pts',(-1.87693852294064,-2.28022456377845,
2.94224716340022E-15));
#21668=CARTESIAN_POINT('Ctrl Pts',(-1.80220903731176,-2.35277040780027,
3.04985240962845E-15));
#21669=CARTESIAN_POINT('Ctrl Pts',(-1.72407227353766,-2.42127570338811,
3.40005801291454E-15));
#21670=CARTESIAN_POINT('Ctrl Pts',(-1.66546970070708,-2.472654675079,3.66271221537911E-15));
#21671=CARTESIAN_POINT('Ctrl Pts',(-1.60494926191777,-2.52176059742133,
2.66897608121856E-15));
#21672=CARTESIAN_POINT('Ctrl Pts',(-1.54263360799992,-2.56844502586205,
2.44249065417534E-15));
#21673=CARTESIAN_POINT('Ctrl Pts',(-1.50966712749181,-2.59314221193751,
2.32267441304543E-15));
#21674=CARTESIAN_POINT('Ctrl Pts',(-1.47619797745247,-2.61716151806854,
2.66421769654117E-15));
#21675=CARTESIAN_POINT('Ctrl Pts',(-1.44224276876128,-2.64047951847467,
2.55351295663786E-15));
#21676=CARTESIAN_POINT('Ctrl Pts',(-1.42523529016054,-2.65215903417213,
2.49806318714802E-15));
#21677=CARTESIAN_POINT('Ctrl Pts',(-1.40811299715223,-2.66365763094131,
1.70970381910793E-15));
#21678=CARTESIAN_POINT('Ctrl Pts',(-1.39088331342309,-2.6749694941009,1.85962356624714E-15));
#21679=CARTESIAN_POINT('Ctrl Pts',(-1.30563836789021,-2.73093564960753,
2.60136095853466E-15));
#21680=CARTESIAN_POINT('Ctrl Pts',(-1.21772994683618,-2.78235951649428,
1.84996893450162E-15));
#21681=CARTESIAN_POINT('Ctrl Pts',(-1.12744127475458,-2.82892568298919,
1.45369827286856E-15));
#21682=CARTESIAN_POINT('Ctrl Pts',(-1.06580182053759,-2.86071608395033,
1.18316702302153E-15));
#21683=CARTESIAN_POINT('Ctrl Pts',(-1.00305209219164,-2.89024190964375,
-1.85681498777599E-15));
#21684=CARTESIAN_POINT('Ctrl Pts',(-0.939272520240859,-2.91739268538644,
-2.72698530423554E-15));
#21685=CARTESIAN_POINT('Ctrl Pts',(-0.891984018423086,-2.93752326119295,
-3.3646306259368E-15));
#21686=CARTESIAN_POINT('Ctrl Pts',(-0.844129218472895,-2.95634804455667,
-1.21993627764454E-15));
#21687=CARTESIAN_POINT('Ctrl Pts',(-0.795758164394645,-2.97388052305262,
-1.30451205393456E-15));
#21688=CARTESIAN_POINT('Ctrl Pts',(-2.51644348201823,0.00207613456667446,
4.11258330249198));
#21689=CARTESIAN_POINT('Ctrl Pts',(-2.51833412820368,0.232035413192547,
4.09805725549862));
#21690=CARTESIAN_POINT('Ctrl Pts',(-2.489317966475,0.461526809188866,4.08353120850527));
#21691=CARTESIAN_POINT('Ctrl Pts',(-2.42745549360351,0.681791335068863,
4.06900516151192));
#21692=CARTESIAN_POINT('Ctrl Pts',(-2.20529160437893,1.47281732314021,4.01683842867202));
#21693=CARTESIAN_POINT('Ctrl Pts',(-1.55950524429922,2.14484335715458,3.96467169583213));
#21694=CARTESIAN_POINT('Ctrl Pts',(-0.777965335250612,2.39835114963567,
3.91250496299223));
#21695=CARTESIAN_POINT('Ctrl Pts',(0.00357457379799905,2.65185894211676,
3.86033823015234));
#21696=CARTESIAN_POINT('Ctrl Pts',(0.920868031815514,2.48684849306456,3.80817149731244));
#21697=CARTESIAN_POINT('Ctrl Pts',(1.56505210920478,1.97685606594732,3.75600476447254));
#21698=CARTESIAN_POINT('Ctrl Pts',(2.20923618659405,1.46686363883008,3.70383803163264));
#21699=CARTESIAN_POINT('Ctrl Pts',(2.58031088335508,0.611889233647789,3.65167129879275));
#21700=CARTESIAN_POINT('Ctrl Pts',(2.51286946562811,-0.206965080676461,
3.59950456595285));
#21701=CARTESIAN_POINT('Ctrl Pts',(2.44542804790114,-1.0258193950007,3.54733783311295));
#21702=CARTESIAN_POINT('Ctrl Pts',(1.93947051568617,-1.80855361846691,3.49517110027306));
#21703=CARTESIAN_POINT('Ctrl Pts',(1.22052364834049,-2.20627780465177,3.44300436743316));
#21704=CARTESIAN_POINT('Ctrl Pts',(0.501576780994809,-2.60400199083662,
3.39083763459327));
#21705=CARTESIAN_POINT('Ctrl Pts',(-0.430359421481595,-2.61671613974014,
3.33867090175337));
#21706=CARTESIAN_POINT('Ctrl Pts',(-1.15988729527642,-2.23875094798029,
3.28650416891347));
#21707=CARTESIAN_POINT('Ctrl Pts',(-1.88941516907125,-1.86078575622044,
3.23433743607358));
#21708=CARTESIAN_POINT('Ctrl Pts',(-2.4165347141845,-1.09214122379723,3.18217070323368));
#21709=CARTESIAN_POINT('Ctrl Pts',(-2.50628827157716,-0.275432188758138,
3.13000397039378));
#21710=CARTESIAN_POINT('Ctrl Pts',(-2.51627910181976,-0.18452101416286,
3.12419708109318));
#21711=CARTESIAN_POINT('Ctrl Pts',(-2.52085061170807,-0.0930142812830837,
3.11839019179258));
#21712=CARTESIAN_POINT('Ctrl Pts',(-2.52021651143941,-0.00144364612508765,
3.11258330249198));
#21713=CARTESIAN_POINT('Ctrl Pts',(-0.793799282532885,-2.96922295374569,
5.));
#21714=CARTESIAN_POINT('Ctrl Pts',(-0.886893974343616,-2.93516849963005,
5.));
#21715=CARTESIAN_POINT('Ctrl Pts',(-0.977926652176332,-2.89635378057927,
5.));
#21716=CARTESIAN_POINT('Ctrl Pts',(-1.06668684681747,-2.85310443912188,
5.));
#21717=CARTESIAN_POINT('Ctrl Pts',(-1.15738407105809,-2.80891125955214,
5.));
#21718=CARTESIAN_POINT('Ctrl Pts',(-1.2457092143346,-2.76008717620201,5.));
#21719=CARTESIAN_POINT('Ctrl Pts',(-1.33140881802392,-2.70693414934569,
5.));
#21720=CARTESIAN_POINT('Ctrl Pts',(-1.4129353161641,-2.65636938639935,5.));
#21721=CARTESIAN_POINT('Ctrl Pts',(-1.49208596169445,-2.60188611256442,
5.));
#21722=CARTESIAN_POINT('Ctrl Pts',(-1.56861084771671,-2.54371537355153,
5.));
#21723=CARTESIAN_POINT('Ctrl Pts',(-1.63557012298619,-2.49281597691525,
5.));
#21724=CARTESIAN_POINT('Ctrl Pts',(-1.70051877227587,-2.43909270266388,
5.));
#21725=CARTESIAN_POINT('Ctrl Pts',(-1.76326584581776,-2.38268809603059,
5.));
#21726=CARTESIAN_POINT('Ctrl Pts',(-1.77895171505325,-2.36858775263627,
5.));
#21727=CARTESIAN_POINT('Ctrl Pts',(-1.79450406853106,-2.35431573679482,
5.));
#21728=CARTESIAN_POINT('Ctrl Pts',(-1.80989576842494,-2.33989703960917,
5.));
#21729=CARTESIAN_POINT('Ctrl Pts',(-1.88231927767376,-2.27205185966276,
5.));
#21730=CARTESIAN_POINT('Ctrl Pts',(-1.95127665379114,-2.20088663840561,
5.));
#21731=CARTESIAN_POINT('Ctrl Pts',(-2.0165263629502,-2.1266887335995,5.));
#21732=CARTESIAN_POINT('Ctrl Pts',(-2.08140824110774,-2.05290910329586,
5.));
#21733=CARTESIAN_POINT('Ctrl Pts',(-2.14262462446156,-1.97613009459816,
5.));
#21734=CARTESIAN_POINT('Ctrl Pts',(-2.19989444056472,-1.89660745904738,
5.));
#21735=CARTESIAN_POINT('Ctrl Pts',(-2.25380452290626,-1.82175001891108,
5.));
#21736=CARTESIAN_POINT('Ctrl Pts',(-2.30421749508371,-1.74446069179507,
5.));
#21737=CARTESIAN_POINT('Ctrl Pts',(-2.35085748563793,-1.66494010874883,
5.));
#21738=CARTESIAN_POINT('Ctrl Pts',(-2.38695950989298,-1.6033866224853,5.));
#21739=CARTESIAN_POINT('Ctrl Pts',(-2.42080014316453,-1.54049593023453,
5.));
#21740=CARTESIAN_POINT('Ctrl Pts',(-2.45223267762586,-1.47635917633043,
5.));
#21741=CARTESIAN_POINT('Ctrl Pts',(-2.45885074786154,-1.46285528460488,
5.));
#21742=CARTESIAN_POINT('Ctrl Pts',(-2.46536230022247,-1.44929534936329,
5.));
#21743=CARTESIAN_POINT('Ctrl Pts',(-2.471759088022,-1.4356951550231,5.));
#21744=CARTESIAN_POINT('Ctrl Pts',(-2.51224453952186,-1.34961913912194,
5.));
#21745=CARTESIAN_POINT('Ctrl Pts',(-2.54820623907542,-1.26179296188141,
5.));
#21746=CARTESIAN_POINT('Ctrl Pts',(-2.57938608018177,-1.17245518793809,
5.));
#21747=CARTESIAN_POINT('Ctrl Pts',(-2.61056592128812,-1.08311741399478,
5.));
#21748=CARTESIAN_POINT('Ctrl Pts',(-2.63696435690728,-0.992267333350395,
5.));
#21749=CARTESIAN_POINT('Ctrl Pts',(-2.65826858221262,-0.900133621000477,
5.));
#21750=CARTESIAN_POINT('Ctrl Pts',(-2.67972778132943,-0.807329698287973,
5.));
#21751=CARTESIAN_POINT('Ctrl Pts',(-2.69601769794397,-0.713222227763925,
5.));
#21752=CARTESIAN_POINT('Ctrl Pts',(-2.70721296581232,-0.618219427263112,
5.));
#21753=CARTESIAN_POINT('Ctrl Pts',(-2.71292220509282,-0.569770946462525,
5.));
#21754=CARTESIAN_POINT('Ctrl Pts',(-2.7173056631566,-0.521089783925043,
5.));
#21755=CARTESIAN_POINT('Ctrl Pts',(-2.7203683315583,-0.472231818984886,
5.));
#21756=CARTESIAN_POINT('Ctrl Pts',(-2.72142997921888,-0.45529562564751,
5.));
#21757=CARTESIAN_POINT('Ctrl Pts',(-2.72233289252141,-0.438338201785387,
5.));
#21758=CARTESIAN_POINT('Ctrl Pts',(-2.72307719183649,-0.421361923846564,
5.));
#21759=CARTESIAN_POINT('Ctrl Pts',(-2.72371459453401,-0.40682378692649,
5.));
#21760=CARTESIAN_POINT('Ctrl Pts',(-2.72423528082335,-0.392280207970546,
5.));
#21761=CARTESIAN_POINT('Ctrl Pts',(-2.72463965223211,-0.3777370307415,5.));
#21762=CARTESIAN_POINT('Ctrl Pts',(-2.7272340736051,-0.284428925823235,
5.));
#21763=CARTESIAN_POINT('Ctrl Pts',(-2.72504745011893,-0.191078680030525,
5.));
#21764=CARTESIAN_POINT('Ctrl Pts',(-2.71820604758435,-0.0980639080872022,
5.));
#21765=CARTESIAN_POINT('Ctrl Pts',(-2.71136148545356,-0.00500617870656192,
5.));
#21766=CARTESIAN_POINT('Ctrl Pts',(-2.69985747016539,0.0877167443723885,
5.));
#21767=CARTESIAN_POINT('Ctrl Pts',(-2.68376992914425,0.179714008003965,
5.));
#21768=CARTESIAN_POINT('Ctrl Pts',(-2.66792655922036,0.27031496919411,5.));
#21769=CARTESIAN_POINT('Ctrl Pts',(-2.64763729016321,0.360212966671102,
5.));
#21770=CARTESIAN_POINT('Ctrl Pts',(-2.62293197139578,0.449008990638608,
5.));
#21771=CARTESIAN_POINT('Ctrl Pts',(-2.61350433154693,0.482893877607947,
5.));
#21772=CARTESIAN_POINT('Ctrl Pts',(-2.60343320797911,0.516617959708256,
5.));
#21773=CARTESIAN_POINT('Ctrl Pts',(-2.5927187899484,0.55015767290499,5.));
#21774=CARTESIAN_POINT('Ctrl Pts',(-2.58640692567121,0.569915919875281,
5.));
#21775=CARTESIAN_POINT('Ctrl Pts',(-2.57987179843875,0.589610167664632,
5.));
#21776=CARTESIAN_POINT('Ctrl Pts',(-2.57311332386527,0.609235450675716,
5.));
#21777=CARTESIAN_POINT('Ctrl Pts',(-2.5676510579122,0.625096798387423,5.));
#21778=CARTESIAN_POINT('Ctrl Pts',(-2.5620452571388,0.640906120496968,5.));
#21779=CARTESIAN_POINT('Ctrl Pts',(-2.55629866051782,0.656654535691256,
5.));
#21780=CARTESIAN_POINT('Ctrl Pts',(-2.52550674415446,0.741039070660769,
5.));
#21781=CARTESIAN_POINT('Ctrl Pts',(-2.4906552842231,0.823736510163055,5.));
#21782=CARTESIAN_POINT('Ctrl Pts',(-2.45179419129016,0.9043762990239,5.));
#21783=CARTESIAN_POINT('Ctrl Pts',(-2.42326911496468,0.963568049912018,
5.));
#21784=CARTESIAN_POINT('Ctrl Pts',(-2.39258278075448,1.0216506842635,5.));
#21785=CARTESIAN_POINT('Ctrl Pts',(-2.35974220291426,1.07846524994913,5.));
#21786=CARTESIAN_POINT('Ctrl Pts',(-2.34707421607123,1.10038100837762,5.));
#21787=CARTESIAN_POINT('Ctrl Pts',(-2.3340855779016,1.12210795474778,5.));
#21788=CARTESIAN_POINT('Ctrl Pts',(-2.32077630204861,1.14363645360599,5.));
#21789=CARTESIAN_POINT('Ctrl Pts',(-2.30811708022228,1.16411345368055,5.));
#21790=CARTESIAN_POINT('Ctrl Pts',(-2.29516494832623,1.18441494534906,5.));
#21791=CARTESIAN_POINT('Ctrl Pts',(-2.28193660666336,1.2045075595742,5.));
#21792=CARTESIAN_POINT('Ctrl Pts',(-2.23464292719215,1.27634223705079,5.));
#21793=CARTESIAN_POINT('Ctrl Pts',(-2.18378817877942,1.34556692931273,5.));
#21794=CARTESIAN_POINT('Ctrl Pts',(-2.12939936247367,1.41182692759809,5.));
#21795=CARTESIAN_POINT('Ctrl Pts',(-2.09060564520546,1.45908796055058,5.));
#21796=CARTESIAN_POINT('Ctrl Pts',(-2.0500132435823,1.504840036578,5.));
#21797=CARTESIAN_POINT('Ctrl Pts',(-2.00762253952656,1.54894112815615,5.));
#21798=CARTESIAN_POINT('Ctrl Pts',(-1.9782483512311,1.57950051132536,5.));
#21799=CARTESIAN_POINT('Ctrl Pts',(-1.94801045703336,1.60926686583501,5.));
#21800=CARTESIAN_POINT('Ctrl Pts',(-1.91694926235925,1.63822229446221,5.));
#21801=CARTESIAN_POINT('Origin',(0.,0.,5.));
#21802=CARTESIAN_POINT('',(2.88675134594813,-5.,5.));
#21803=CARTESIAN_POINT('',(5.77350269189626,0.,5.));
#21804=CARTESIAN_POINT('',(2.88675134594813,-5.,5.));
#21805=CARTESIAN_POINT('',(2.88675134594813,5.,5.));
#21806=CARTESIAN_POINT('',(5.77350269189626,0.,5.));
#21807=CARTESIAN_POINT('',(-2.88675134594813,5.,5.));
#21808=CARTESIAN_POINT('',(2.88675134594813,5.,5.));
#21809=CARTESIAN_POINT('',(-5.77350269189626,1.11022302462516E-15,5.));
#21810=CARTESIAN_POINT('',(-2.88675134594813,5.,5.));
#21811=CARTESIAN_POINT('',(-2.88675134594813,-5.,5.));
#21812=CARTESIAN_POINT('',(-5.77350269189626,7.07050159149938E-16,5.));
#21813=CARTESIAN_POINT('',(-2.88675134594813,-5.,5.));
#21814=CARTESIAN_POINT('Origin',(0.,0.,2.5));
#21815=CARTESIAN_POINT('Origin',(-2.88675134594813,-5.,0.));
#21816=CARTESIAN_POINT('',(-2.88675134594813,-5.,0.));
#21817=CARTESIAN_POINT('',(2.88675134594813,-5.,0.));
#21818=CARTESIAN_POINT('',(-2.88675134594813,-5.,0.));
#21819=CARTESIAN_POINT('',(2.88675134594813,-5.,0.));
#21820=CARTESIAN_POINT('',(-2.88675134594813,-5.,0.));
#21821=CARTESIAN_POINT('Origin',(-5.77350269189626,7.07050159149938E-16,
0.));
#21822=CARTESIAN_POINT('',(-5.77350269189626,7.07050159149938E-16,0.));
#21823=CARTESIAN_POINT('',(-5.77350269189626,7.07050159149938E-16,0.));
#21824=CARTESIAN_POINT('',(-5.77350269189626,7.07050159149938E-16,0.));
#21825=CARTESIAN_POINT('Origin',(-2.88675134594813,5.,0.));
#21826=CARTESIAN_POINT('',(-2.88675134594813,5.,0.));
#21827=CARTESIAN_POINT('',(-2.88675134594813,5.,0.));
#21828=CARTESIAN_POINT('',(-2.88675134594813,5.,0.));
#21829=CARTESIAN_POINT('Origin',(2.88675134594813,5.,0.));
#21830=CARTESIAN_POINT('',(2.88675134594813,5.,0.));
#21831=CARTESIAN_POINT('',(2.88675134594813,5.,0.));
#21832=CARTESIAN_POINT('',(2.88675134594813,5.,0.));
#21833=CARTESIAN_POINT('Origin',(5.77350269189626,0.,0.));
#21834=CARTESIAN_POINT('',(5.77350269189626,0.,0.));
#21835=CARTESIAN_POINT('',(5.77350269189626,0.,0.));
#21836=CARTESIAN_POINT('',(5.77350269189626,0.,0.));
#21837=CARTESIAN_POINT('Origin',(2.88675134594813,-5.,0.));
#21838=CARTESIAN_POINT('',(2.88675134594813,-5.,0.));
#21839=CARTESIAN_POINT('Origin',(0.,0.,0.));
#21867=UNCERTAINTY_MEASURE_WITH_UNIT(LENGTH_MEASURE(0.01),#21881,
'DISTANCE_ACCURACY_VALUE',
'Maximum model space distance between geometric entities at asserted c
onnectivities');
#21868=UNCERTAINTY_MEASURE_WITH_UNIT(LENGTH_MEASURE(0.01),#21881,
'DISTANCE_ACCURACY_VALUE',
'Maximum model space distance between geometric entities at asserted c
onnectivities');
#21879=(
GEOMETRIC_REPRESENTATION_CONTEXT(3)
GLOBAL_UNCERTAINTY_ASSIGNED_CONTEXT((#21867))
GLOBAL_UNIT_ASSIGNED_CONTEXT((#21881,#21883,#21884))
REPRESENTATION_CONTEXT('','3D')
);
#21880=(
GEOMETRIC_REPRESENTATION_CONTEXT(3)
GLOBAL_UNCERTAINTY_ASSIGNED_CONTEXT((#21868))
GLOBAL_UNIT_ASSIGNED_CONTEXT((#21881,#21883,#21884))
REPRESENTATION_CONTEXT('','3D')
);
#21881=(
LENGTH_UNIT()
NAMED_UNIT(*)
SI_UNIT(.MILLI.,.METRE.)
);
#21883=(
NAMED_UNIT(*)
PLANE_ANGLE_UNIT()
SI_UNIT($,.RADIAN.)
);
#21884=(
NAMED_UNIT(*)
SI_UNIT($,.STERADIAN.)
SOLID_ANGLE_UNIT()
);
#21895=SHAPE_DEFINITION_REPRESENTATION(#21906,#21934);
#21906=PRODUCT_DEFINITION_SHAPE('',$,#21946);
#21934=SHAPE_REPRESENTATION('',(#6925),#21879);
#21935=PRODUCT_DEFINITION_CONTEXT('part definition',#21970,'design');
#21946=PRODUCT_DEFINITION('Hex nut M6','Hex nut M6',#21957,#21935);
#21957=PRODUCT_DEFINITION_FORMATION('',$,#21982);
#21970=APPLICATION_CONTEXT(
'Core Data for Automotive Mechanical Design Process');
#21971=PRODUCT_CONTEXT('part definition',#21970,'mechanical');
#21982=PRODUCT('Hex nut M6','Hex nut M6',$,(#21971));
#21985=PRESENTATION_STYLE_ASSIGNMENT((#21991));
#21991=SURFACE_STYLE_USAGE(.BOTH.,#21997);
#21997=SURFACE_SIDE_STYLE('',(#22003));
#22003=SURFACE_STYLE_FILL_AREA(#22009);
#22009=FILL_AREA_STYLE('Gray',(#22015));
#22015=FILL_AREA_STYLE_COLOUR('Gray',#22021);
#22021=COLOUR_RGB('Gray',0.407843137254902,0.447058823529412,0.498039215686275);
ENDSEC;
END-ISO-10303-21;
